ISO-10303-21;
HEADER;
FILE_DESCRIPTION (('STEP AP214'),
    '1' );
FILE_NAME ('4-Axle(Cross).step',
    '2026-10-28T16:50:19',
    ( '' ),
    ( '' ),
    'SwSTEP 2.0',
    'SolidWorks 2024',
    '' );
FILE_SCHEMA (( 'AUTOMOTIVE_DESIGN' ));
ENDSEC;

DATA;
#3=FACE_OUTER_BOUND ( 'NONE', #2882, .T. ) ;
#5=EDGE_LOOP ( 'NONE', ( #4798, #3652 ) ) ;
#11=LINE ( 'NONE', #2843, #879 ) ;
#25=DIRECTION ( 'NONE',  ( -1.000000000000000000, 0.000000000000000000, 0.000000000000000000 ) ) ;
#35=CARTESIAN_POINT ( 'NONE',  ( 28.50000000000000355, 7.347880794884122694E-16, 5.000000000000000000 ) ) ;
#67=FACE_OUTER_BOUND ( 'NONE', #9174, .T. ) ;
#68=CYLINDRICAL_SURFACE ( 'NONE', #4244, 3.000000000000000000 ) ;
#80=AXIS2_PLACEMENT_3D ( 'NONE', #2507, #6973, #1060 ) ;
#83=DIRECTION ( 'NONE',  ( 1.224646799147353207E-16, 1.000000000000000000, -0.000000000000000000 ) ) ;
#86=EDGE_LOOP ( 'NONE', ( #7800, #8743 ) ) ;
#87=CARTESIAN_POINT ( 'NONE',  ( -19.50000000000000355, 3.673940397442054445E-16, 5.000000000000000000 ) ) ;
#90=CARTESIAN_POINT ( 'NONE',  ( 6.702350214711367826, 26.42345776824586423, 0.2543657081580636414 ) ) ;
#117=AXIS2_PLACEMENT_3D ( 'NONE', #9182, #529, #8560 ) ;
#118=CARTESIAN_POINT ( 'NONE',  ( -28.50000000000000355, 0.000000000000000000, 5.000000000000000000 ) ) ;
#129=CYLINDRICAL_SURFACE ( 'NONE', #8083, 3.000000000000000000 ) ;
#136=ORIENTED_EDGE ( 'NONE', *, *, #6818, .T. ) ;
#141=ADVANCED_FACE ( 'NONE', ( #2217 ), #5149, .T. ) ;
#145=EDGE_CURVE ( 'NONE', #5577, #3040, #1032, .T. ) ;
#148=VECTOR ( 'NONE', #6018, 1000.000000000000114 ) ;
#152=VERTEX_POINT ( 'NONE', #8316 ) ;
#177=AXIS2_PLACEMENT_3D ( 'NONE', #643, #6371, #687 ) ;
#185=CYLINDRICAL_SURFACE ( 'NONE', #862, 3.000000000000000000 ) ;
#187=DIRECTION ( 'NONE',  ( -1.000000000000000000, 0.000000000000000000, 0.000000000000000000 ) ) ;
#194=EDGE_CURVE ( 'NONE', #5380, #7603, #3025, .T. ) ;
#197=EDGE_LOOP ( 'NONE', ( #6623, #3215, #8581, #5552 ) ) ;
#209=ORIENTED_EDGE ( 'NONE', *, *, #5661, .T. ) ;
#212=DIRECTION ( 'NONE',  ( -0.000000000000000000, -0.000000000000000000, -1.000000000000000000 ) ) ;
#214=CIRCLE ( 'NONE', #1119, 2.999999999999999112 ) ;
#226=CARTESIAN_POINT ( 'NONE',  ( 13.50000000000000178, 0.000000000000000000, 27.50000000000000355 ) ) ;
#236=CONICAL_SURFACE ( 'NONE', #4063, 14.49999999999998401, 0.7853981633974533860 ) ;
#237=ORIENTED_EDGE ( 'NONE', *, *, #1949, .T. ) ;
#241=DIRECTION ( 'NONE',  ( 1.000000000000000000, 0.000000000000000000, 0.000000000000000000 ) ) ;
#259=LINE ( 'NONE', #9083, #2418 ) ;
#275=VECTOR ( 'NONE', #434, 1000.000000000000000 ) ;
#277=VECTOR ( 'NONE', #4768, 1000.000000000000000 ) ;
#284=LINE ( 'NONE', #8259, #4546 ) ;
#285=DIRECTION ( 'NONE',  ( 0.000000000000000000, 0.000000000000000000, -1.000000000000000000 ) ) ;
#288=DIRECTION ( 'NONE',  ( 0.000000000000000000, 0.000000000000000000, -1.000000000000000000 ) ) ;
#291=CARTESIAN_POINT ( 'NONE',  ( 5.103771271004210242, -27.45068023253072909, 0.9147230066269097515 ) ) ;
#300=CARTESIAN_POINT ( 'NONE',  ( -26.42320443315921352, 6.702656137449878315, 0.2542028498880767873 ) ) ;
#308=EDGE_CURVE ( 'NONE', #4536, #5331, #8465, .T. ) ;
#315=DIRECTION ( 'NONE',  ( 1.000000000000000000, 0.000000000000000000, 0.000000000000000000 ) ) ;
#338=AXIS2_PLACEMENT_3D ( 'NONE', #1148, #4717, #3174 ) ;
#341=CARTESIAN_POINT ( 'NONE',  ( 6.000000000000000888, 22.50000000000000355, 2.000000000000013767 ) ) ;
#344=ORIENTED_EDGE ( 'NONE', *, *, #1475, .F. ) ;
#346=ORIENTED_EDGE ( 'NONE', *, *, #7933, .F. ) ;
#354=ORIENTED_EDGE ( 'NONE', *, *, #1055, .F. ) ;
#355=EDGE_LOOP ( 'NONE', ( #5445, #2395, #8124, #5569 ) ) ;
#371=ORIENTED_EDGE ( 'NONE', *, *, #6027, .F. ) ;
#373=VECTOR ( 'NONE', #8630, 1000.000000000000000 ) ;
#376=ORIENTED_EDGE ( 'NONE', *, *, #2647, .T. ) ;
#380=CARTESIAN_POINT ( 'NONE',  ( 0.000000000000000000, -22.50000000000000355, 0.000000000000000000 ) ) ;
#382=FACE_OUTER_BOUND ( 'NONE', #2751, .T. ) ;
#386=VERTEX_POINT ( 'NONE', #3317 ) ;
#393=DIRECTION ( 'NONE',  ( 0.000000000000000000, 0.000000000000000000, 1.000000000000000000 ) ) ;
#399=ORIENTED_EDGE ( 'NONE', *, *, #3163, .F. ) ;
#401=LINE ( 'NONE', #6284, #5327 ) ;
#404=CIRCLE ( 'NONE', #2411, 11.96410161513786008 ) ;
#415=FACE_OUTER_BOUND ( 'NONE', #1978, .T. ) ;
#419=EDGE_CURVE ( 'NONE', #5419, #3913, #3949, .T. ) ;
#420=LINE ( 'NONE', #3394, #982 ) ;
#431=CIRCLE ( 'NONE', #2590, 6.000000000000000888 ) ;
#432=DIRECTION ( 'NONE',  ( -0.000000000000000000, -0.000000000000000000, -1.000000000000000000 ) ) ;
#434=DIRECTION ( 'NONE',  ( -0.000000000000000000, -0.000000000000000000, -1.000000000000000000 ) ) ;
#449=ORIENTED_EDGE ( 'NONE', *, *, #3589, .T. ) ;
#450=VERTEX_POINT ( 'NONE', #87 ) ;
#462=EDGE_CURVE ( 'NONE', #5577, #4499, #9447, .T. ) ;
#464=DIRECTION ( 'NONE',  ( 0.000000000000000000, 0.000000000000000000, -1.000000000000000000 ) ) ;
#470=CARTESIAN_POINT ( 'NONE',  ( 28.21791960234944341, 3.296518076058924773, 1.407948315796077488 ) ) ;
#488=EDGE_CURVE ( 'NONE', #9116, #6136, #6414, .T. ) ;
#496=DIRECTION ( 'NONE',  ( 0.000000000000000000, 0.000000000000000000, 1.000000000000000000 ) ) ;
#500=CIRCLE ( 'NONE', #2957, 8.000000000000021316 ) ;
#501=CARTESIAN_POINT ( 'NONE',  ( 22.50000000000000355, 0.000000000000000000, 10.00000000000000000 ) ) ;
#506=CARTESIAN_POINT ( 'NONE',  ( 0.000000000000000000, -22.50000000000000355, 10.00000000000000000 ) ) ;
#513=CARTESIAN_POINT ( 'NONE',  ( 28.66635145370233673, 1.351859493328352091, 1.696225934522933132 ) ) ;
#525=AXIS2_PLACEMENT_3D ( 'NONE', #6666, #83, #3007 ) ;
#529=DIRECTION ( 'NONE',  ( 0.000000000000000000, 0.000000000000000000, -1.000000000000000000 ) ) ;
#533=FACE_OUTER_BOUND ( 'NONE', #4151, .T. ) ;
#540=EDGE_CURVE ( 'NONE', #4866, #6634, #4500, .T. ) ;
#541=ORIENTED_EDGE ( 'NONE', *, *, #549, .F. ) ;
#544=DIRECTION ( 'NONE',  ( -0.000000000000000000, -0.000000000000000000, -1.000000000000000000 ) ) ;
#548=ORIENTED_EDGE ( 'NONE', *, *, #1293, .T. ) ;
#549=EDGE_CURVE ( 'NONE', #1368, #849, #2819, .T. ) ;
#556=ADVANCED_FACE ( 'NONE', ( #2453, #6048, #4749, #8968, #2397, #5469 ), #3297, .T. ) ;
#561=CARTESIAN_POINT ( 'NONE',  ( -7.180166011355011868, -26.02777777777776791, 0.000000000000000000 ) ) ;
#571=CARTESIAN_POINT ( 'NONE',  ( 0.000000000000000000, 22.50000000000000355, 5.000000000000000000 ) ) ;
#576=ORIENTED_EDGE ( 'NONE', *, *, #1236, .F. ) ;
#578=EDGE_LOOP ( 'NONE', ( #1745, #6700, #5279, #2448 ) ) ;
#589=AXIS2_PLACEMENT_3D ( 'NONE', #8025, #3797, #1585 ) ;
#594=EDGE_CURVE ( 'NONE', #5792, #8082, #284, .T. ) ;
#598=EDGE_CURVE ( 'NONE', #3092, #1471, #8300, .T. ) ;
#606=DIRECTION ( 'NONE',  ( 1.000000000000000000, 0.000000000000000000, 0.000000000000000000 ) ) ;
#613=EDGE_CURVE ( 'NONE', #2492, #9459, #3813, .T. ) ;
#614=ORIENTED_EDGE ( 'NONE', *, *, #5661, .F. ) ;
#615=ORIENTED_EDGE ( 'NONE', *, *, #540, .F. ) ;
#630=CARTESIAN_POINT ( 'NONE',  ( 0.000000000000000000, 22.50000000000000355, 0.000000000000000000 ) ) ;
#637=ORIENTED_EDGE ( 'NONE', *, *, #2315, .F. ) ;
#643=CARTESIAN_POINT ( 'NONE',  ( 0.000000000000000000, 22.50000000000000355, 5.000000000000000000 ) ) ;
#646=DIRECTION ( 'NONE',  ( 0.000000000000000000, 0.000000000000000000, -1.000000000000000000 ) ) ;
#650=VECTOR ( 'NONE', #212, 1000.000000000000000 ) ;
#651=VERTEX_POINT ( 'NONE', #8582 ) ;
#655=CARTESIAN_POINT ( 'NONE',  ( -3.000000000000000000, 22.50000000000000355, 10.00000000000000000 ) ) ;
#661=ORIENTED_EDGE ( 'NONE', *, *, #8541, .F. ) ;
#662=VERTEX_POINT ( 'NONE', #4972 ) ;
#670=EDGE_LOOP ( 'NONE', ( #399, #371, #4638, #1647, #934, #6701, #9260, #4002 ) ) ;
#672=VERTEX_POINT ( 'NONE', #7860 ) ;
#678=FACE_BOUND ( 'NONE', #2572, .T. ) ;
#686=CARTESIAN_POINT ( 'NONE',  ( 22.50000000000000355, 0.000000000000000000, 10.00000000000000000 ) ) ;
#687=DIRECTION ( 'NONE',  ( -1.000000000000000000, 0.000000000000000000, 0.000000000000000000 ) ) ;
#703=VERTEX_POINT ( 'NONE', #9244 ) ;
#709=EDGE_CURVE ( 'NONE', #4100, #933, #6475, .T. ) ;
#713=EDGE_CURVE ( 'NONE', #5539, #1940, #902, .T. ) ;
#715=CARTESIAN_POINT ( 'NONE',  ( 22.50000000000000355, 0.000000000000000000, 2.000000000000035083 ) ) ;
#716=ORIENTED_EDGE ( 'NONE', *, *, #2046, .F. ) ;
#722=CARTESIAN_POINT ( 'NONE',  ( -15.00000000000000000, 0.000000000000000000, 26.99999999999999289 ) ) ;
#724=VECTOR ( 'NONE', #985, 1000.000000000000000 ) ;
#726=VECTOR ( 'NONE', #8362, 1000.000000000000000 ) ;
#735=ORIENTED_EDGE ( 'NONE', *, *, #8413, .T. ) ;
#739=DIRECTION ( 'NONE',  ( 0.000000000000000000, 0.000000000000000000, 1.000000000000000000 ) ) ;
#742=DIRECTION ( 'NONE',  ( 0.000000000000000000, 0.000000000000000000, 1.000000000000000000 ) ) ;
#743=ORIENTED_EDGE ( 'NONE', *, *, #6480, .T. ) ;
#767=DIRECTION ( 'NONE',  ( -1.000000000000000000, 0.000000000000000000, 0.000000000000000000 ) ) ;
#769=LINE ( 'NONE', #3702, #4981 ) ;
#774=EDGE_CURVE ( 'NONE', #2124, #5549, #7816, .T. ) ;
#793=ORIENTED_EDGE ( 'NONE', *, *, #7002, .F. ) ;
#799=CARTESIAN_POINT ( 'NONE',  ( -7.180166011355011868, 26.02777777777776436, 0.000000000000000000 ) ) ;
#810=DIRECTION ( 'NONE',  ( -1.000000000000000000, 0.000000000000000000, 0.000000000000000000 ) ) ;
#832=ORIENTED_EDGE ( 'NONE', *, *, #4823, .T. ) ;
#833=( NAMED_UNIT ( * ) PLANE_ANGLE_UNIT ( ) SI_UNIT ( $, .RADIAN. ) );
#834=ORIENTED_EDGE ( 'NONE', *, *, #6458, .T. ) ;
#838=CONICAL_SURFACE ( 'NONE', #2540, 6.000000000000000888, 0.7853981633974498333 ) ;
#849=VERTEX_POINT ( 'NONE', #7325 ) ;
#851=CARTESIAN_POINT ( 'NONE',  ( -6.186958832529963814, 26.79406326810229189, 0.4926121009229034176 ) ) ;
#853=PRODUCT_DEFINITION_CONTEXT ( 'detailed design', #8359, 'design' ) ;
#860=CARTESIAN_POINT ( 'NONE',  ( 16.50000000000000000, 0.000000000000000000, 2.000000000000035083 ) ) ;
#862=AXIS2_PLACEMENT_3D ( 'NONE', #5379, #2493, #7676 ) ;
#866=LINE ( 'NONE', #6548, #148 ) ;
#868=DIRECTION ( 'NONE',  ( -0.000000000000000000, -0.000000000000000000, -1.000000000000000000 ) ) ;
#871=CIRCLE ( 'NONE', #7781, 6.000000000000001776 ) ;
#879=VECTOR ( 'NONE', #1538, 1000.000000000000000 ) ;
#897=DIRECTION ( 'NONE',  ( -1.000000000000000000, 0.000000000000000000, 0.000000000000000000 ) ) ;
#902=CIRCLE ( 'NONE', #3664, 3.000000000000000000 ) ;
#911=ORIENTED_EDGE ( 'NONE', *, *, #8809, .F. ) ;
#933=VERTEX_POINT ( 'NONE', #1749 ) ;
#934=ORIENTED_EDGE ( 'NONE', *, *, #1402, .F. ) ;
#940=CARTESIAN_POINT ( 'NONE',  ( 3.000000000000000000, -22.50000000000000355, 5.000000000000000000 ) ) ;
#942=DIRECTION ( 'NONE',  ( 1.000000000000000000, 0.000000000000000000, 0.000000000000000000 ) ) ;
#948=ORIENTED_EDGE ( 'NONE', *, *, #1475, .T. ) ;
#954=CARTESIAN_POINT ( 'NONE',  ( -2.323800269068097446, -28.49052126930483197, 1.583192244553113914 ) ) ;
#972=AXIS2_PLACEMENT_3D ( 'NONE', #1152, #1063, #8364 ) ;
#976=ORIENTED_EDGE ( 'NONE', *, *, #3071, .T. ) ;
#982=VECTOR ( 'NONE', #3353, 1000.000000000000000 ) ;
#983=DIRECTION ( 'NONE',  ( 0.2588190451025176309, 3.169619151431726731E-17, -0.9659258262890692004 ) ) ;
#985=DIRECTION ( 'NONE',  ( -0.000000000000000000, -0.000000000000000000, -1.000000000000000000 ) ) ;
#987=ORIENTED_EDGE ( 'NONE', *, *, #6818, .F. ) ;
#988=CIRCLE ( 'NONE', #6517, 6.000000000000001776 ) ;
#994=CIRCLE ( 'NONE', #6372, 26.99999999999999645 ) ;
#1013=CARTESIAN_POINT ( 'NONE',  ( -27.86926932341927809, 4.210987672173478025, 1.183815993626686991 ) ) ;
#1032=CIRCLE ( 'NONE', #3186, 6.000000000000000888 ) ;
#1034=CIRCLE ( 'NONE', #7314, 2.999999999999999112 ) ;
#1042=FACE_OUTER_BOUND ( 'NONE', #4857, .T. ) ;
#1051=CARTESIAN_POINT ( 'NONE',  ( -4.208878922505766340, -27.87018698802495464, 1.184405920873192075 ) ) ;
#1053=AXIS2_PLACEMENT_3D ( 'NONE', #5638, #7795, #1348 ) ;
#1055=EDGE_CURVE ( 'NONE', #8953, #9116, #866, .T. ) ;
#1060=DIRECTION ( 'NONE',  ( -1.000000000000000000, 0.000000000000000000, -0.000000000000000000 ) ) ;
#1063=DIRECTION ( 'NONE',  ( 0.000000000000000000, 0.000000000000000000, -1.000000000000000000 ) ) ;
#1087=ORIENTED_EDGE ( 'NONE', *, *, #3711, .F. ) ;
#1088=DIRECTION ( 'NONE',  ( -1.000000000000000000, 0.000000000000000000, 0.000000000000000000 ) ) ;
#1097=ADVANCED_FACE ( 'NONE', ( #678, #4378 ), #8749, .T. ) ;
#1108=DIRECTION ( 'NONE',  ( 0.000000000000000000, 0.000000000000000000, 1.000000000000000000 ) ) ;
#1119=AXIS2_PLACEMENT_3D ( 'NONE', #4301, #646, #2135 ) ;
#1133=CARTESIAN_POINT ( 'NONE',  ( 0.000000000000000000, -22.50000000000000355, 5.000000000000000000 ) ) ;
#1134=AXIS2_PLACEMENT_3D ( 'NONE', #6917, #5385, #7630 ) ;
#1142=CARTESIAN_POINT ( 'NONE',  ( -4.506465992502256768, -27.73646215562212092, 1.098439957185652682 ) ) ;
#1144=ORIENTED_EDGE ( 'NONE', *, *, #4830, .F. ) ;
#1148=CARTESIAN_POINT ( 'NONE',  ( 0.000000000000000000, 22.50000000000000355, 2.000000000000013767 ) ) ;
#1152=CARTESIAN_POINT ( 'NONE',  ( 22.50000000000000355, 0.000000000000000000, 5.000000000000000000 ) ) ;
#1154=EDGE_LOOP ( 'NONE', ( #4904, #2784, #3254, #4832, #3865, #3227 ) ) ;
#1155=CARTESIAN_POINT ( 'NONE',  ( -15.00000000000000000, 0.000000000000000000, 10.00000000000000000 ) ) ;
#1159=CARTESIAN_POINT ( 'NONE',  ( 0.000000000000000000, -22.50000000000000355, 0.000000000000000000 ) ) ;
#1166=CARTESIAN_POINT ( 'NONE',  ( 0.000000000000000000, 0.000000000000000000, 0.000000000000000000 ) ) ;
#1168=CONICAL_SURFACE ( 'NONE', #7456, 30.00000000000000000, 0.7853981633974488341 ) ;
#1172=CARTESIAN_POINT ( 'NONE',  ( -22.50000000000000355, 0.000000000000000000, 2.000000000000039080 ) ) ;
#1187=AXIS2_PLACEMENT_3D ( 'NONE', #9074, #8215, #4762 ) ;
#1189=CARTESIAN_POINT ( 'NONE',  ( 27.45147183906050969, 5.102343880922168395, 0.9152318965389144578 ) ) ;
#1190=EDGE_CURVE ( 'NONE', #5539, #5419, #4669, .T. ) ;
#1196=DIRECTION ( 'NONE',  ( -1.000000000000000000, 0.000000000000000000, 0.000000000000000000 ) ) ;
#1199=ORIENTED_EDGE ( 'NONE', *, *, #8949, .T. ) ;
#1214=DIRECTION ( 'NONE',  ( 1.000000000000000000, 0.000000000000000000, 0.000000000000000000 ) ) ;
#1222=DIRECTION ( 'NONE',  ( 0.000000000000000000, 0.000000000000000000, 1.000000000000000000 ) ) ;
#1225=CARTESIAN_POINT ( 'NONE',  ( -6.000000000000000888, -22.50000000000000355, 5.000000000000000000 ) ) ;
#1230=CARTESIAN_POINT ( 'NONE',  ( 28.40723282374007042, 2.660173739710351981, 1.529649672404342242 ) ) ;
#1236=EDGE_CURVE ( 'NONE', #7815, #2124, #3224, .T. ) ;
#1246=CARTESIAN_POINT ( 'NONE',  ( -25.50000000000000355, 0.000000000000000000, 10.00000000000000000 ) ) ;
#1251=DIRECTION ( 'NONE',  ( -1.000000000000000000, 0.000000000000000000, 0.000000000000000000 ) ) ;
#1254=ORIENTED_EDGE ( 'NONE', *, *, #9320, .F. ) ;
#1267=CARTESIAN_POINT ( 'NONE',  ( -16.50000000000000000, 7.347880794884122694E-16, 2.000000000000039080 ) ) ;
#1271=VECTOR ( 'NONE', #868, 1000.000000000000000 ) ;
#1272=DIRECTION ( 'NONE',  ( -0.000000000000000000, -0.000000000000000000, 1.000000000000000000 ) ) ;
#1274=CARTESIAN_POINT ( 'NONE',  ( 26.42790562391195053, 6.696979066941341152, 0.2572250439434040636 ) ) ;
#1276=ORIENTED_EDGE ( 'NONE', *, *, #3071, .F. ) ;
#1280=CIRCLE ( 'NONE', #1134, 6.000000000000000888 ) ;
#1281=DIRECTION ( 'NONE',  ( -0.000000000000000000, -0.000000000000000000, -1.000000000000000000 ) ) ;
#1288=EDGE_CURVE ( 'NONE', #8082, #2348, #2509, .T. ) ;
#1293=EDGE_CURVE ( 'NONE', #7976, #5380, #6870, .T. ) ;
#1304=DIRECTION ( 'NONE',  ( 0.000000000000000000, 0.000000000000000000, -1.000000000000000000 ) ) ;
#1318=DIRECTION ( 'NONE',  ( -1.000000000000000000, 0.000000000000000000, 0.000000000000000000 ) ) ;
#1322=( GEOMETRIC_REPRESENTATION_CONTEXT ( 3 ) GLOBAL_UNCERTAINTY_ASSIGNED_CONTEXT ( ( #3073 ) ) GLOBAL_UNIT_ASSIGNED_CONTEXT ( ( #6901, #7607, #6034 ) ) REPRESENTATION_CONTEXT ( 'NONE', 'WORKASPACE' ) );
#1338=CARTESIAN_POINT ( 'NONE',  ( -28.50000000000000355, 0.000000000000000000, 5.000000000000000000 ) ) ;
#1348=DIRECTION ( 'NONE',  ( 1.000000000000000000, 0.000000000000000000, 0.000000000000000000 ) ) ;
#1353=ORIENTED_EDGE ( 'NONE', *, *, #8809, .T. ) ;
#1356=ORIENTED_EDGE ( 'NONE', *, *, #4938, .F. ) ;
#1365=ORIENTED_EDGE ( 'NONE', *, *, #8414, .F. ) ;
#1368=VERTEX_POINT ( 'NONE', #9259 ) ;
#1384=CARTESIAN_POINT ( 'NONE',  ( 3.000000000000000000, 22.50000000000000355, 10.00000000000000000 ) ) ;
#1395=CARTESIAN_POINT ( 'NONE',  ( -27.74194578790376653, -4.529188556225802742, 1.101965149366714192 ) ) ;
#1402=EDGE_CURVE ( 'NONE', #6136, #8845, #5647, .T. ) ;
#1410=AXIS2_PLACEMENT_3D ( 'NONE', #8798, #8847, #3041 ) ;
#1413=EDGE_CURVE ( 'NONE', #5812, #6191, #2694, .T. ) ;
#1423=ORIENTED_EDGE ( 'NONE', *, *, #4319, .T. ) ;
#1424=ORIENTED_EDGE ( 'NONE', *, *, #7147, .T. ) ;
#1447=ORIENTED_EDGE ( 'NONE', *, *, #8984, .T. ) ;
#1451=CARTESIAN_POINT ( 'NONE',  ( 0.000000000000000000, 0.000000000000000000, 10.00000000000000000 ) ) ;
#1457=CIRCLE ( 'NONE', #3172, 8.000000000000021316 ) ;
#1459=DIRECTION ( 'NONE',  ( 0.000000000000000000, 0.000000000000000000, 1.000000000000000000 ) ) ;
#1471=VERTEX_POINT ( 'NONE', #4507 ) ;
#1475=EDGE_CURVE ( 'NONE', #7481, #1766, #2921, .T. ) ;
#1512=LINE ( 'NONE', #35, #8565 ) ;
#1519=CARTESIAN_POINT ( 'NONE',  ( -22.50000000000000355, 0.000000000000000000, 5.000000000000000000 ) ) ;
#1528=UNCERTAINTY_MEASURE_WITH_UNIT (LENGTH_MEASURE( 1.000000000000000082E-05 ), #5211, 'distance_accuracy_value', 'NONE');
#1538=DIRECTION ( 'NONE',  ( -0.000000000000000000, -0.000000000000000000, -1.000000000000000000 ) ) ;
#1541=DIRECTION ( 'NONE',  ( -1.000000000000000000, 0.000000000000000000, 0.000000000000000000 ) ) ;
#1550=ADVANCED_FACE ( 'NONE', ( #6629 ), #9466, .T. ) ;
#1555=EDGE_LOOP ( 'NONE', ( #5705, #6411, #9134, #661 ) ) ;
#1560=CARTESIAN_POINT ( 'NONE',  ( -3.000000000000000000, 22.50000000000000355, 10.00000000000000000 ) ) ;
#1575=CARTESIAN_POINT ( 'NONE',  ( 2.323800269068097446, 28.49052126930483197, 1.583192244553113914 ) ) ;
#1576=EDGE_CURVE ( 'NONE', #3936, #672, #8702, .T. ) ;
#1583=AXIS2_PLACEMENT_3D ( 'NONE', #1133, #6773, #187 ) ;
#1585=DIRECTION ( 'NONE',  ( -1.000000000000000000, 0.000000000000000000, 0.000000000000000000 ) ) ;
#1586=AXIS2_PLACEMENT_3D ( 'NONE', #4601, #3875, #7614 ) ;
#1595=ADVANCED_FACE ( 'NONE', ( #7291 ), #8399, .F. ) ;
#1596=ADVANCED_FACE ( 'NONE', ( #3 ), #1796, .F. ) ;
#1602=ORIENTED_EDGE ( 'NONE', *, *, #1413, .T. ) ;
#1603=AXIS2_PLACEMENT_3D ( 'NONE', #2769, #7852, #5107 ) ;
#1605=ORIENTED_EDGE ( 'NONE', *, *, #4812, .T. ) ;
#1614=AXIS2_PLACEMENT_3D ( 'NONE', #6760, #5504, #4539 ) ;
#1624=CARTESIAN_POINT ( 'NONE',  ( 2.651740589948411664, 28.40946940741335069, 1.531087476194299413 ) ) ;
#1633=ADVANCED_FACE ( 'NONE', ( #6008 ), #6918, .T. ) ;
#1642=CARTESIAN_POINT ( 'NONE',  ( 0.000000000000000000, 0.000000000000000000, 27.50000000000000355 ) ) ;
#1643=CARTESIAN_POINT ( 'NONE',  ( -16.50000000000000000, 7.347880794884122694E-16, 5.000000000000000000 ) ) ;
#1647=ORIENTED_EDGE ( 'NONE', *, *, #1717, .F. ) ;
#1651=AXIS2_PLACEMENT_3D ( 'NONE', #6202, #8402, #1769 ) ;
#1680=AXIS2_PLACEMENT_3D ( 'NONE', #7354, #8080, #4431 ) ;
#1688=CYLINDRICAL_SURFACE ( 'NONE', #1187, 6.000000000000001776 ) ;
#1690=CARTESIAN_POINT ( 'NONE',  ( 13.50000000000000178, 0.000000000000000000, 28.50000000000000355 ) ) ;
#1695=CARTESIAN_POINT ( 'NONE',  ( 12.50000000000000000, 1.530808498934191127E-15, 50.00000000000000000 ) ) ;
#1707=FACE_OUTER_BOUND ( 'NONE', #670, .T. ) ;
#1713=EDGE_CURVE ( 'NONE', #3455, #7998, #2734, .T. ) ;
#1717=EDGE_CURVE ( 'NONE', #8845, #4404, #3137, .T. ) ;
#1722=CIRCLE ( 'NONE', #8611, 8.000000000000021316 ) ;
#1723=CARTESIAN_POINT ( 'NONE',  ( 3.600085285568724203, 28.11218154377481682, 1.339973849569531472 ) ) ;
#1725=CARTESIAN_POINT ( 'NONE',  ( 0.000000000000000000, 0.000000000000000000, 50.00000000000000000 ) ) ;
#1745=ORIENTED_EDGE ( 'NONE', *, *, #598, .F. ) ;
#1749=CARTESIAN_POINT ( 'NONE',  ( -14.49999999999995381, 9.797174393178884822E-16, 0.000000000000000000 ) ) ;
#1751=DIRECTION ( 'NONE',  ( -1.000000000000000000, 0.000000000000000000, 0.000000000000000000 ) ) ;
#1756=CARTESIAN_POINT ( 'NONE',  ( 0.000000000000000000, 22.50000000000000355, 5.000000000000000000 ) ) ;
#1758=CARTESIAN_POINT ( 'NONE',  ( 0.000000000000000000, 0.000000000000000000, 48.00000000000036948 ) ) ;
#1766=VERTEX_POINT ( 'NONE', #4269 ) ;
#1769=DIRECTION ( 'NONE',  ( -1.000000000000000000, 0.000000000000000000, 0.000000000000000000 ) ) ;
#1780=CARTESIAN_POINT ( 'NONE',  ( -28.48969330601477168, 2.327370969396575617, 1.582659982438082036 ) ) ;
#1781=EDGE_LOOP ( 'NONE', ( #4751, #7391, #2761, #5715, #4013 ) ) ;
#1786=DIRECTION ( 'NONE',  ( -0.000000000000000000, -0.000000000000000000, -1.000000000000000000 ) ) ;
#1796=CONICAL_SURFACE ( 'NONE', #5487, 6.000000000000001776, 0.7853981633974431720 ) ;
#1801=CARTESIAN_POINT ( 'NONE',  ( 11.96410161513786008, 1.465179874765226021E-15, 50.00000000000000000 ) ) ;
#1805=CARTESIAN_POINT ( 'NONE',  ( 28.68405123480337693, -1.339801352072190310, 1.707604365230744659 ) ) ;
#1810=LINE ( 'NONE', #7527, #8521 ) ;
#1814=EDGE_LOOP ( 'NONE', ( #8597, #6397, #7503, #8647 ) ) ;
#1815=ADVANCED_FACE ( 'NONE', ( #9204 ), #8454, .F. ) ;
#1830=CARTESIAN_POINT ( 'NONE',  ( 0.000000000000000000, 0.000000000000000000, 27.50000000000000355 ) ) ;
#1831=EDGE_CURVE ( 'NONE', #849, #2124, #7034, .T. ) ;
#1854=LINE ( 'NONE', #1801, #5698 ) ;
#1865=DIRECTION ( 'NONE',  ( 1.000000000000000000, 0.000000000000000000, 0.000000000000000000 ) ) ;
#1867=DIRECTION ( 'NONE',  ( -0.000000000000000000, -0.000000000000000000, -1.000000000000000000 ) ) ;
#1888=CARTESIAN_POINT ( 'NONE',  ( -30.00000000000000000, 3.673940397442059178E-15, 2.999999999999999112 ) ) ;
#1889=EDGE_CURVE ( 'NONE', #4158, #7322, #3798, .T. ) ;
#1893=ORIENTED_EDGE ( 'NONE', *, *, #7002, .T. ) ;
#1896=CARTESIAN_POINT ( 'NONE',  ( 0.000000000000000000, 0.000000000000000000, 2.999999999999999112 ) ) ;
#1901=ORIENTED_EDGE ( 'NONE', *, *, #2046, .T. ) ;
#1911=CARTESIAN_POINT ( 'NONE',  ( -26.02777777777775370, 7.180166011355047395, 0.000000000000000000 ) ) ;
#1919=CARTESIAN_POINT ( 'NONE',  ( 14.49999999999998579, 0.000000000000000000, 0.000000000000000000 ) ) ;
#1921=FACE_OUTER_BOUND ( 'NONE', #1154, .T. ) ;
#1932=CARTESIAN_POINT ( 'NONE',  ( 3.000000000000000000, 22.50000000000000355, 10.00000000000000000 ) ) ;
#1940=VERTEX_POINT ( 'NONE', #2293 ) ;
#1946=CARTESIAN_POINT ( 'NONE',  ( 30.00000000000000000, 3.673940397442059178E-15, 2.999999999999999112 ) ) ;
#1947=CYLINDRICAL_SURFACE ( 'NONE', #7408, 2.999999999999999112 ) ;
#1948=ORIENTED_EDGE ( 'NONE', *, *, #4142, .T. ) ;
#1949=EDGE_CURVE ( 'NONE', #3236, #3951, #4050, .T. ) ;
#1952=AXIS2_PLACEMENT_3D ( 'NONE', #5784, #8084, #4437 ) ;
#1955=CIRCLE ( 'NONE', #2260, 3.000000000000000000 ) ;
#1961=EDGE_CURVE ( 'NONE', #2124, #6136, #5194, .T. ) ;
#1967=CARTESIAN_POINT ( 'NONE',  ( 27.74194578790375587, 4.529188556225775208, 1.101965149366711971 ) ) ;
#1972=CARTESIAN_POINT ( 'NONE',  ( 0.000000000000000000, 0.000000000000000000, 0.000000000000000000 ) ) ;
#1978=EDGE_LOOP ( 'NONE', ( #4055, #1948, #716, #1144 ) ) ;
#1980=FACE_OUTER_BOUND ( 'NONE', #8222, .T. ) ;
#1993=CARTESIAN_POINT ( 'NONE',  ( -7.180166011355011868, -26.02777777777776791, 0.000000000000000000 ) ) ;
#2005=CARTESIAN_POINT ( 'NONE',  ( -19.50000000000000355, 3.673940397442056417E-16, 10.00000000000000000 ) ) ;
#2006=CIRCLE ( 'NONE', #9203, 8.000000000000017764 ) ;
#2012=ADVANCED_FACE ( 'NONE', ( #3826 ), #3063, .F. ) ;
#2014=DIRECTION ( 'NONE',  ( 1.000000000000000000, 0.000000000000000000, 0.000000000000000000 ) ) ;
#2029=CARTESIAN_POINT ( 'NONE',  ( -26.42790562391193987, -6.696979066941380232, 0.2572250439434045632 ) ) ;
#2037=DIRECTION ( 'NONE',  ( 1.000000000000000000, 0.000000000000000000, -0.000000000000000000 ) ) ;
#2040=DIRECTION ( 'NONE',  ( 0.000000000000000000, 0.000000000000000000, -1.000000000000000000 ) ) ;
#2044=FACE_BOUND ( 'NONE', #9387, .T. ) ;
#2046=EDGE_CURVE ( 'NONE', #7322, #4158, #6507, .T. ) ;
#2048=DIRECTION ( 'NONE',  ( 0.7071067811865512365, 8.659560562354979697E-17, -0.7071067811865439090 ) ) ;
#2049=AXIS2_PLACEMENT_3D ( 'NONE', #4606, #9064, #2496 ) ;
#2090=DIRECTION ( 'NONE',  ( 1.000000000000000000, 0.000000000000000000, 0.000000000000000000 ) ) ;
#2106=AXIS2_PLACEMENT_3D ( 'NONE', #4794, #3302, #1865 ) ;
#2112=ADVANCED_FACE ( 'NONE', ( #4646 ), #7570, .F. ) ;
#2118=DIRECTION ( 'NONE',  ( -1.000000000000000000, 0.000000000000000000, 0.000000000000000000 ) ) ;
#2124=VERTEX_POINT ( 'NONE', #7672 ) ;
#2135=DIRECTION ( 'NONE',  ( -1.000000000000000000, 0.000000000000000000, 0.000000000000000000 ) ) ;
#2143=EDGE_CURVE ( 'NONE', #7322, #4945, #7084, .T. ) ;
#2153=VECTOR ( 'NONE', #6479, 1000.000000000000000 ) ;
#2163=CARTESIAN_POINT ( 'NONE',  ( 7.180166011355011868, -26.02777777777776436, 0.000000000000000000 ) ) ;
#2176=CARTESIAN_POINT ( 'NONE',  ( 0.000000000000000000, 0.000000000000000000, 27.50000000000000355 ) ) ;
#2182=ORIENTED_EDGE ( 'NONE', *, *, #594, .F. ) ;
#2186=EDGE_CURVE ( 'NONE', #4100, #6191, #5884, .T. ) ;
#2188=LINE ( 'NONE', #655, #2153 ) ;
#2190=CYLINDRICAL_SURFACE ( 'NONE', #8204, 2.999999999999999112 ) ;
#2193=DIRECTION ( 'NONE',  ( 1.000000000000000000, 0.000000000000000000, 0.000000000000000000 ) ) ;
#2202=EDGE_LOOP ( 'NONE', ( #3842, #5725, #948, #3193 ) ) ;
#2208=FACE_OUTER_BOUND ( 'NONE', #8058, .T. ) ;
#2215=CARTESIAN_POINT ( 'NONE',  ( -22.50000000000000355, 0.000000000000000000, 10.00000000000000000 ) ) ;
#2217=FACE_OUTER_BOUND ( 'NONE', #3708, .T. ) ;
#2237=ADVANCED_FACE ( 'NONE', ( #8531 ), #1947, .F. ) ;
#2241=AXIS2_PLACEMENT_3D ( 'NONE', #1166, #496, #2037 ) ;
#2247=CARTESIAN_POINT ( 'NONE',  ( -3.614752790974351981, 28.10687131109265735, 1.336560128559570959 ) ) ;
#2255=EDGE_CURVE ( 'NONE', #3092, #7550, #9405, .T. ) ;
#2260=AXIS2_PLACEMENT_3D ( 'NONE', #4342, #8946, #7312 ) ;
#2266=AXIS2_PLACEMENT_3D ( 'NONE', #5172, #8870, #2193 ) ;
#2274=DIRECTION ( 'NONE',  ( 1.000000000000000000, 0.000000000000000000, 0.000000000000000000 ) ) ;
#2291=CARTESIAN_POINT ( 'NONE',  ( 25.50000000000000355, 3.673940397442054445E-16, 5.000000000000000000 ) ) ;
#2293=CARTESIAN_POINT ( 'NONE',  ( -3.000000000000000000, -22.50000000000000355, 10.00000000000000000 ) ) ;
#2303=EDGE_CURVE ( 'NONE', #7086, #4536, #214, .T. ) ;
#2305=ADVANCED_FACE ( 'NONE', ( #3572 ), #5144, .F. ) ;
#2314=DIRECTION ( 'NONE',  ( -0.000000000000000000, -0.000000000000000000, 1.000000000000000000 ) ) ;
#2315=EDGE_CURVE ( 'NONE', #703, #4100, #7448, .T. ) ;
#2316=CARTESIAN_POINT ( 'NONE',  ( 6.000000000000000888, -22.50000000000000355, 5.000000000000000000 ) ) ;
#2328=EDGE_CURVE ( 'NONE', #4422, #5465, #9248, .T. ) ;
#2337=EDGE_LOOP ( 'NONE', ( #6995, #4484, #4817, #4224, #6540 ) ) ;
#2343=DIRECTION ( 'NONE',  ( 0.000000000000000000, 0.000000000000000000, -1.000000000000000000 ) ) ;
#2346=CARTESIAN_POINT ( 'NONE',  ( 28.21952111405551022, -3.291689805591845541, 1.408977859035689617 ) ) ;
#2348=VERTEX_POINT ( 'NONE', #2468 ) ;
#2350=DIRECTION ( 'NONE',  ( 1.000000000000000000, 0.000000000000000000, 0.000000000000000000 ) ) ;
#2354=CARTESIAN_POINT ( 'NONE',  ( -3.299340129088522922, 28.21697752735853726, 1.407342696159064488 ) ) ;
#2365=AXIS2_PLACEMENT_3D ( 'NONE', #8680, #5036, #7968 ) ;
#2371=EDGE_CURVE ( 'NONE', #651, #3742, #6434, .T. ) ;
#2376=LINE ( 'NONE', #8319, #3952 ) ;
#2382=EDGE_LOOP ( 'NONE', ( #2827, #2922, #8455, #1199 ) ) ;
#2391=( GEOMETRIC_REPRESENTATION_CONTEXT ( 3 ) GLOBAL_UNCERTAINTY_ASSIGNED_CONTEXT ( ( #1528 ) ) GLOBAL_UNIT_ASSIGNED_CONTEXT ( ( #5211, #833, #5886 ) ) REPRESENTATION_CONTEXT ( 'NONE', 'WORKASPACE' ) );
#2393=CARTESIAN_POINT ( 'NONE',  ( 27.44426127775442126, -5.090287965588936814, 0.9105965356992768989 ) ) ;
#2395=ORIENTED_EDGE ( 'NONE', *, *, #9460, .F. ) ;
#2396=ORIENTED_EDGE ( 'NONE', *, *, #4998, .F. ) ;
#2397=FACE_BOUND ( 'NONE', #5749, .T. ) ;
#2404=CARTESIAN_POINT ( 'NONE',  ( -1.335553917663280021, -28.68463450227767453, 1.707979322892793306 ) ) ;
#2411=AXIS2_PLACEMENT_3D ( 'NONE', #7320, #742, #4487 ) ;
#2418=VECTOR ( 'NONE', #3858, 1000.000000000000000 ) ;
#2423=VECTOR ( 'NONE', #5957, 1000.000000000000000 ) ;
#2433=EDGE_CURVE ( 'NONE', #3688, #5331, #4954, .T. ) ;
#2440=FACE_OUTER_BOUND ( 'NONE', #2337, .T. ) ;
#2448=ORIENTED_EDGE ( 'NONE', *, *, #7232, .T. ) ;
#2453=FACE_BOUND ( 'NONE', #4235, .T. ) ;
#2457=VECTOR ( 'NONE', #5394, 1000.000000000000114 ) ;
#2459=CARTESIAN_POINT ( 'NONE',  ( 3.614752790974351981, -28.10687131109265735, 1.336560128559570959 ) ) ;
#2468=CARTESIAN_POINT ( 'NONE',  ( 8.000000000000021316, 22.50000000000000355, 0.000000000000000000 ) ) ;
#2470=ORIENTED_EDGE ( 'NONE', *, *, #1949, .F. ) ;
#2475=EDGE_CURVE ( 'NONE', #4866, #5577, #9258, .T. ) ;
#2488=DIRECTION ( 'NONE',  ( 0.000000000000000000, 0.000000000000000000, -1.000000000000000000 ) ) ;
#2489=CARTESIAN_POINT ( 'NONE',  ( -3.000000000000000000, 22.50000000000000355, 5.000000000000000000 ) ) ;
#2492=VERTEX_POINT ( 'NONE', #1384 ) ;
#2493=DIRECTION ( 'NONE',  ( -0.000000000000000000, -0.000000000000000000, -1.000000000000000000 ) ) ;
#2496=DIRECTION ( 'NONE',  ( 1.000000000000000000, 1.776356839400250465E-15, 0.000000000000000000 ) ) ;
#2501=FACE_OUTER_BOUND ( 'NONE', #2382, .T. ) ;
#2502=CARTESIAN_POINT ( 'NONE',  ( 0.3423334138323023135, -28.74982858564768762, 1.749889805059230419 ) ) ;
#2507=CARTESIAN_POINT ( 'NONE',  ( 0.000000000000000000, -22.50000000000000355, 5.000000000000000000 ) ) ;
#2509=LINE ( 'NONE', #341, #726 ) ;
#2532=CARTESIAN_POINT ( 'NONE',  ( 26.42320443315922063, -6.702656137449844564, 0.2542028498880765097 ) ) ;
#2534=EDGE_LOOP ( 'NONE', ( #5986, #5234 ) ) ;
#2540=AXIS2_PLACEMENT_3D ( 'NONE', #7395, #3750, #7352 ) ;
#2545=CARTESIAN_POINT ( 'NONE',  ( 0.000000000000000000, 0.000000000000000000, 10.00000000000000000 ) ) ;
#2556=DIRECTION ( 'NONE',  ( 0.000000000000000000, -1.000000000000000000, 0.000000000000000000 ) ) ;
#2559=ADVANCED_FACE ( 'NONE', ( #1921 ), #3424, .F. ) ;
#2572=EDGE_LOOP ( 'NONE', ( #2470, #6825 ) ) ;
#2580=CIRCLE ( 'NONE', #2106, 12.50000000000000000 ) ;
#2590=AXIS2_PLACEMENT_3D ( 'NONE', #4607, #285, #7679 ) ;
#2606=PLANE ( 'NONE',  #80 ) ;
#2608=CARTESIAN_POINT ( 'NONE',  ( -27.73557521625266276, 4.508354841688235304, 1.097869781876724238 ) ) ;
#2625=VECTOR ( 'NONE', #3927, 1000.000000000000000 ) ;
#2643=CARTESIAN_POINT ( 'NONE',  ( 28.10782586465402488, 3.612161042402800781, 1.337173770134738371 ) ) ;
#2647=EDGE_CURVE ( 'NONE', #4404, #7651, #7426, .T. ) ;
#2657=ORIENTED_EDGE ( 'NONE', *, *, #1402, .T. ) ;
#2694=LINE ( 'NONE', #1338, #275 ) ;
#2705=PRODUCT ( '4-Axle(Cross)', '4-Axle(Cross)', '', ( #9117 ) ) ;
#2706=CARTESIAN_POINT ( 'NONE',  ( -28.48725673979378570, -2.337639529181975817, 1.581093618438872195 ) ) ;
#2712=DIRECTION ( 'NONE',  ( 1.000000000000000000, 0.000000000000000000, 0.000000000000000000 ) ) ;
#2716=FACE_OUTER_BOUND ( 'NONE', #1555, .T. ) ;
#2728=CARTESIAN_POINT ( 'NONE',  ( 0.000000000000000000, 22.50000000000000355, 10.00000000000000000 ) ) ;
#2732=AXIS2_PLACEMENT_3D ( 'NONE', #4274, #8064, #2014 ) ;
#2733=CARTESIAN_POINT ( 'NONE',  ( 3.000000000000000000, 22.50000000000000355, 5.000000000000000000 ) ) ;
#2734=CIRCLE ( 'NONE', #6275, 11.96410161513786008 ) ;
#2735=CIRCLE ( 'NONE', #9012, 2.999999999999999112 ) ;
#2737=DIRECTION ( 'NONE',  ( 0.000000000000000000, 0.000000000000000000, -1.000000000000000000 ) ) ;
#2744=DIRECTION ( 'NONE',  ( 1.000000000000000000, 0.000000000000000000, 0.000000000000000000 ) ) ;
#2748=DIRECTION ( 'NONE',  ( -0.000000000000000000, -0.000000000000000000, -1.000000000000000000 ) ) ;
#2751=EDGE_LOOP ( 'NONE', ( #2906, #3966 ) ) ;
#2755=DIRECTION ( 'NONE',  ( 1.000000000000000000, 0.000000000000000000, -0.000000000000000000 ) ) ;
#2758=CARTESIAN_POINT ( 'NONE',  ( -26.02777777777775370, -7.180166011355047395, 0.000000000000000000 ) ) ;
#2761=ORIENTED_EDGE ( 'NONE', *, *, #2944, .T. ) ;
#2766=EDGE_CURVE ( 'NONE', #6634, #4866, #1280, .T. ) ;
#2768=LINE ( 'NONE', #7949, #4312 ) ;
#2769=CARTESIAN_POINT ( 'NONE',  ( -22.50000000000000355, 0.000000000000000000, 5.000000000000000000 ) ) ;
#2774=EDGE_LOOP ( 'NONE', ( #5885, #9364 ) ) ;
#2784=ORIENTED_EDGE ( 'NONE', *, *, #462, .T. ) ;
#2785=APPLICATION_CONTEXT ( 'automotive_design' ) ;
#2799=CARTESIAN_POINT ( 'NONE',  ( -28.73308667824889540, -0.6789743538665677924, 1.739127150302868463 ) ) ;
#2812=EDGE_LOOP ( 'NONE', ( #7167, #136, #1893, #3376 ) ) ;
#2819=CIRCLE ( 'NONE', #2049, 26.99999999999999645 ) ;
#2822=VECTOR ( 'NONE', #7718, 1000.000000000000000 ) ;
#2827=ORIENTED_EDGE ( 'NONE', *, *, #8231, .F. ) ;
#2832=ADVANCED_FACE ( 'NONE', ( #2501 ), #5428, .T. ) ;
#2833=AXIS2_PLACEMENT_3D ( 'NONE', #1756, #2488, #3245 ) ;
#2835=ADVANCED_FACE ( 'NONE', ( #5474 ), #8959, .T. ) ;
#2843=CARTESIAN_POINT ( 'NONE',  ( -6.000000000000000888, 22.50000000000000355, 5.000000000000000000 ) ) ;
#2854=CARTESIAN_POINT ( 'NONE',  ( -6.000000000000000888, -22.50000000000000355, 5.000000000000000000 ) ) ;
#2856=DIRECTION ( 'NONE',  ( -0.7071067811865486830, 0.000000000000000000, -0.7071067811865464625 ) ) ;
#2882=EDGE_LOOP ( 'NONE', ( #793, #4613, #3052, #4181, #354 ) ) ;
#2904=DIRECTION ( 'NONE',  ( -1.000000000000000000, 0.000000000000000000, 0.000000000000000000 ) ) ;
#2906=ORIENTED_EDGE ( 'NONE', *, *, #2766, .T. ) ;
#2912=DIRECTION ( 'NONE',  ( -1.000000000000000000, 0.000000000000000000, 0.000000000000000000 ) ) ;
#2921=LINE ( 'NONE', #4323, #2423 ) ;
#2922=ORIENTED_EDGE ( 'NONE', *, *, #1576, .F. ) ;
#2930=CARTESIAN_POINT ( 'NONE',  ( 22.50000000000000355, 0.000000000000000000, 5.000000000000000000 ) ) ;
#2939=PRODUCT_DEFINITION ( 'UNKNOWN', '', #9276, #853 ) ;
#2944=EDGE_CURVE ( 'NONE', #6191, #651, #420, .T. ) ;
#2957=AXIS2_PLACEMENT_3D ( 'NONE', #6087, #6185, #7563 ) ;
#2959=EDGE_CURVE ( 'NONE', #5812, #703, #7887, .T. ) ;
#2964=EDGE_CURVE ( 'NONE', #152, #450, #8586, .T. ) ;
#2970=DIRECTION ( 'NONE',  ( -1.000000000000000000, 0.000000000000000000, 0.000000000000000000 ) ) ;
#2974=ORIENTED_EDGE ( 'NONE', *, *, #6168, .F. ) ;
#2977=DIRECTION ( 'NONE',  ( 0.000000000000000000, 0.000000000000000000, -1.000000000000000000 ) ) ;
#2989=DIRECTION ( 'NONE',  ( -1.000000000000000000, 0.000000000000000000, 0.000000000000000000 ) ) ;
#3007=DIRECTION ( 'NONE',  ( -1.000000000000000000, 1.224646799147353454E-16, 0.000000000000000000 ) ) ;
#3019=TOROIDAL_SURFACE ( 'NONE', #5494, 13.50000000000000178, 1.000000000000000000 ) ;
#3025=CIRCLE ( 'NONE', #7022, 13.50000000000000178 ) ;
#3029=DIRECTION ( 'NONE',  ( -1.000000000000000000, 0.000000000000000000, 0.000000000000000000 ) ) ;
#3031=DIRECTION ( 'NONE',  ( -0.000000000000000000, -0.000000000000000000, -1.000000000000000000 ) ) ;
#3040=VERTEX_POINT ( 'NONE', #6717 ) ;
#3041=DIRECTION ( 'NONE',  ( -1.000000000000000000, 0.000000000000000000, 0.000000000000000000 ) ) ;
#3052=ORIENTED_EDGE ( 'NONE', *, *, #1961, .T. ) ;
#3058=DIRECTION ( 'NONE',  ( -0.000000000000000000, -0.000000000000000000, -1.000000000000000000 ) ) ;
#3059=AXIS2_PLACEMENT_3D ( 'NONE', #6844, #4005, #4813 ) ;
#3061=CARTESIAN_POINT ( 'NONE',  ( 14.49999999999998401, 1.806354028742345013E-15, 27.50000000000000355 ) ) ;
#3063=CYLINDRICAL_SURFACE ( 'NONE', #1586, 6.000000000000000888 ) ;
#3065=EDGE_LOOP ( 'NONE', ( #615, #3463, #6505, #3674 ) ) ;
#3071=EDGE_CURVE ( 'NONE', #703, #5812, #988, .T. ) ;
#3073=UNCERTAINTY_MEASURE_WITH_UNIT (LENGTH_MEASURE( 1.000000000000000082E-05 ), #6901, 'distance_accuracy_value', 'NONE');
#3075=ORIENTED_EDGE ( 'NONE', *, *, #2371, .F. ) ;
#3076=ORIENTED_EDGE ( 'NONE', *, *, #2433, .F. ) ;
#3078=CARTESIAN_POINT ( 'NONE',  ( 0.000000000000000000, 22.50000000000000355, 5.000000000000000000 ) ) ;
#3091=CARTESIAN_POINT ( 'NONE',  ( 0.000000000000000000, -22.50000000000000355, 0.000000000000000000 ) ) ;
#3092=VERTEX_POINT ( 'NONE', #3776 ) ;
#3101=CIRCLE ( 'NONE', #338, 6.000000000000000888 ) ;
#3109=ORIENTED_EDGE ( 'NONE', *, *, #3426, .F. ) ;
#3124=DIRECTION ( 'NONE',  ( -1.000000000000000000, 0.000000000000000000, 0.000000000000000000 ) ) ;
#3134=AXIS2_PLACEMENT_3D ( 'NONE', #3488, #1272, #6339 ) ;
#3137=B_SPLINE_CURVE_WITH_KNOTS ( 'NONE', 3,
 ( #9023, #3840, #6873, #291, #3214, #2459, #7631, #8208, #4562, #6158, #7487, #3165, #2502, #7539, #2404, #954, #6822, #5386, #5429, #1051, #1142, #9160, #8631, #6387, #4891, #561 ),
 .UNSPECIFIED., .F., .F.,
 ( 4, 2, 2, 2, 2, 2, 2, 2, 2, 2, 2, 2, 4 ),
 ( 1.812491582141323212E-18, 0.002002306497011713607, 0.004004612994023425479, 0.005005766242529281415, 0.006006919491035139086, 0.007008072739540995022, 0.008009225988046852693, 0.01001153248505856456, 0.01101268573356442224, 0.01201383898207027817, 0.01301499223057613411, 0.01401614547908198831, 0.01601845197609370539 ),
 .UNSPECIFIED. ) ;
#3139=EDGE_CURVE ( 'NONE', #4945, #7603, #6827, .T. ) ;
#3154=LINE ( 'NONE', #1888, #4366 ) ;
#3157=ORIENTED_EDGE ( 'NONE', *, *, #6652, .F. ) ;
#3161=ORIENTED_EDGE ( 'NONE', *, *, #9436, .T. ) ;
#3163=EDGE_CURVE ( 'NONE', #651, #9261, #3154, .T. ) ;
#3165=CARTESIAN_POINT ( 'NONE',  ( 0.6837532375831764098, -28.73276100836656610, 1.738917791092793319 ) ) ;
#3172=AXIS2_PLACEMENT_3D ( 'NONE', #5069, #1459, #8766 ) ;
#3174=DIRECTION ( 'NONE',  ( 1.000000000000000000, 0.000000000000000000, 0.000000000000000000 ) ) ;
#3178=VERTEX_POINT ( 'NONE', #7751 ) ;
#3181=EDGE_LOOP ( 'NONE', ( #7722, #9133, #548, #3109 ) ) ;
#3186=AXIS2_PLACEMENT_3D ( 'NONE', #3756, #6839, #8136 ) ;
#3193=ORIENTED_EDGE ( 'NONE', *, *, #7399, .T. ) ;
#3214=CARTESIAN_POINT ( 'NONE',  ( 4.531045531831497719, -27.74104493317181053, 1.101386028467601141 ) ) ;
#3215=ORIENTED_EDGE ( 'NONE', *, *, #6649, .T. ) ;
#3220=CARTESIAN_POINT ( 'NONE',  ( -22.50000000000000355, 0.000000000000000000, 0.000000000000000000 ) ) ;
#3222=EDGE_CURVE ( 'NONE', #3936, #9261, #5548, .T. ) ;
#3224=LINE ( 'NONE', #6262, #2457 ) ;
#3225=DIRECTION ( 'NONE',  ( 0.000000000000000000, 0.000000000000000000, 1.000000000000000000 ) ) ;
#3227=ORIENTED_EDGE ( 'NONE', *, *, #8571, .F. ) ;
#3236=VERTEX_POINT ( 'NONE', #2489 ) ;
#3245=DIRECTION ( 'NONE',  ( -1.000000000000000000, 0.000000000000000000, 0.000000000000000000 ) ) ;
#3249=ORIENTED_EDGE ( 'NONE', *, *, #7638, .T. ) ;
#3254=ORIENTED_EDGE ( 'NONE', *, *, #9208, .F. ) ;
#3260=CARTESIAN_POINT ( 'NONE',  ( 22.50000000000000355, 0.000000000000000000, 2.000000000000035083 ) ) ;
#3269=AXIS2_PLACEMENT_3D ( 'NONE', #1830, #3225, #5395 ) ;
#3277=AXIS2_PLACEMENT_3D ( 'NONE', #1758, #4693, #942 ) ;
#3278=FACE_OUTER_BOUND ( 'NONE', #5671, .T. ) ;
#3284=ORIENTED_EDGE ( 'NONE', *, *, #2475, .F. ) ;
#3297=PLANE ( 'NONE',  #6244 ) ;
#3302=DIRECTION ( 'NONE',  ( 0.000000000000000000, 0.000000000000000000, 1.000000000000000000 ) ) ;
#3317=CARTESIAN_POINT ( 'NONE',  ( 28.50000000000000355, 7.347880794884123680E-16, 5.000000000000000000 ) ) ;
#3332=CARTESIAN_POINT ( 'NONE',  ( 0.000000000000000000, 0.000000000000000000, 28.50000000000000355 ) ) ;
#3342=DIRECTION ( 'NONE',  ( 1.000000000000000000, 0.000000000000000000, 0.000000000000000000 ) ) ;
#3343=ORIENTED_EDGE ( 'NONE', *, *, #4297, .T. ) ;
#3344=ORIENTED_EDGE ( 'NONE', *, *, #1055, .T. ) ;
#3353=DIRECTION ( 'NONE',  ( -0.7071067811865487940, 0.000000000000000000, -0.7071067811865463515 ) ) ;
#3359=EDGE_CURVE ( 'NONE', #152, #7481, #6108, .T. ) ;
#3362=ADVANCED_FACE ( 'NONE', ( #3754 ), #4248, .T. ) ;
#3363=DIRECTION ( 'NONE',  ( -0.000000000000000000, -0.000000000000000000, -1.000000000000000000 ) ) ;
#3373=DIRECTION ( 'NONE',  ( 1.000000000000000000, 0.000000000000000000, 0.000000000000000000 ) ) ;
#3376=ORIENTED_EDGE ( 'NONE', *, *, #6480, .F. ) ;
#3378=FACE_OUTER_BOUND ( 'NONE', #3181, .T. ) ;
#3394=CARTESIAN_POINT ( 'NONE',  ( -28.50000000000000355, 0.000000000000000000, 2.000000000000039080 ) ) ;
#3405=ORIENTED_EDGE ( 'NONE', *, *, #2255, .F. ) ;
#3406=AXIS2_PLACEMENT_3D ( 'NONE', #5495, #8425, #3808 ) ;
#3424=CONICAL_SURFACE ( 'NONE', #5735, 6.000000000000000888, 0.7853981633974498333 ) ;
#3426=EDGE_CURVE ( 'NONE', #7603, #5380, #4099, .T. ) ;
#3441=CARTESIAN_POINT ( 'NONE',  ( 28.73308667824889184, 0.6789743538665647948, 1.739127150302864244 ) ) ;
#3448=DIRECTION ( 'NONE',  ( 0.000000000000000000, 0.000000000000000000, -1.000000000000000000 ) ) ;
#3455=VERTEX_POINT ( 'NONE', #7973 ) ;
#3463=ORIENTED_EDGE ( 'NONE', *, *, #2475, .T. ) ;
#3473=DIRECTION ( 'NONE',  ( -0.000000000000000000, -0.000000000000000000, -1.000000000000000000 ) ) ;
#3481=DIRECTION ( 'NONE',  ( 0.000000000000000000, 0.000000000000000000, -1.000000000000000000 ) ) ;
#3488=CARTESIAN_POINT ( 'NONE',  ( 0.000000000000000000, 0.000000000000000000, 2.999999999999999112 ) ) ;
#3497=CIRCLE ( 'NONE', #589, 6.000000000000001776 ) ;
#3530=EDGE_CURVE ( 'NONE', #6191, #4100, #6874, .T. ) ;
#3535=ADVANCED_FACE ( 'NONE', ( #4320 ), #3019, .F. ) ;
#3537=DIRECTION ( 'NONE',  ( 0.000000000000000000, 0.000000000000000000, -1.000000000000000000 ) ) ;
#3551=DIRECTION ( 'NONE',  ( -0.000000000000000000, -0.000000000000000000, -1.000000000000000000 ) ) ;
#3552=AXIS2_PLACEMENT_3D ( 'NONE', #8605, #4146, #1251 ) ;
#3559=DIRECTION ( 'NONE',  ( 1.000000000000000000, 0.000000000000000000, 0.000000000000000000 ) ) ;
#3562=AXIS2_PLACEMENT_3D ( 'NONE', #9277, #5648, #7989 ) ;
#3568=AXIS2_PLACEMENT_3D ( 'NONE', #3332, #7215, #2712 ) ;
#3572=FACE_OUTER_BOUND ( 'NONE', #5101, .T. ) ;
#3574=AXIS2_PLACEMENT_3D ( 'NONE', #6071, #2040, #7898 ) ;
#3576=CARTESIAN_POINT ( 'NONE',  ( -6.000000000000000888, 22.50000000000000355, 5.000000000000000000 ) ) ;
#3589=EDGE_CURVE ( 'NONE', #662, #1368, #5879, .T. ) ;
#3592=DIRECTION ( 'NONE',  ( 0.000000000000000000, 0.000000000000000000, 1.000000000000000000 ) ) ;
#3602=CARTESIAN_POINT ( 'NONE',  ( 22.50000000000000355, 0.000000000000000000, 5.000000000000000000 ) ) ;
#3616=FACE_OUTER_BOUND ( 'NONE', #578, .T. ) ;
#3617=FACE_OUTER_BOUND ( 'NONE', #3723, .T. ) ;
#3635=CLOSED_SHELL ( 'NONE', ( #5435, #3535, #3819, #2835, #4996, #8218, #2559, #1596, #9222, #5256, #8451, #2237, #5258, #9050, #1815, #4920, #141, #4341, #1633, #2832, #556, #8289, #7130, #9414, #6021, #7464, #7648, #8697, #2012, #5042, #4657, #7124, #7748, #1097, #2305, #8057, #5241, #2112, #1595, #3893, #6359, #8879, #8235, #1550, #7105, #3362 ) ) ;
#3638=EDGE_LOOP ( 'NONE', ( #1365, #5442, #5398, #1254 ) ) ;
#3641=FACE_OUTER_BOUND ( 'NONE', #1781, .T. ) ;
#3648=CARTESIAN_POINT ( 'NONE',  ( 0.000000000000000000, 0.000000000000000000, 0.000000000000000000 ) ) ;
#3649=DIRECTION ( 'NONE',  ( 0.000000000000000000, 0.000000000000000000, -1.000000000000000000 ) ) ;
#3652=ORIENTED_EDGE ( 'NONE', *, *, #8414, .T. ) ;
#3664=AXIS2_PLACEMENT_3D ( 'NONE', #506, #3481, #1318 ) ;
#3670=DIRECTION ( 'NONE',  ( 0.000000000000000000, 0.000000000000000000, -1.000000000000000000 ) ) ;
#3674=ORIENTED_EDGE ( 'NONE', *, *, #7147, .F. ) ;
#3682=CYLINDRICAL_SURFACE ( 'NONE', #6520, 2.999999999999999112 ) ;
#3688=VERTEX_POINT ( 'NONE', #9020 ) ;
#3692=CARTESIAN_POINT ( 'NONE',  ( 0.000000000000000000, 0.000000000000000000, 10.00000000000000000 ) ) ;
#3698=CARTESIAN_POINT ( 'NONE',  ( -26.02777777777775370, -7.180166011355047395, 0.000000000000000000 ) ) ;
#3702=CARTESIAN_POINT ( 'NONE',  ( -3.000000000000000000, -22.50000000000000355, 10.00000000000000000 ) ) ;
#3708=EDGE_LOOP ( 'NONE', ( #1901, #6311, #832, #3719 ) ) ;
#3711=EDGE_CURVE ( 'NONE', #4945, #7976, #2580, .T. ) ;
#3719=ORIENTED_EDGE ( 'NONE', *, *, #2143, .F. ) ;
#3723=EDGE_LOOP ( 'NONE', ( #4121, #6996, #3954, #2396 ) ) ;
#3736=DIRECTION ( 'NONE',  ( 0.000000000000000000, 0.000000000000000000, -1.000000000000000000 ) ) ;
#3738=CARTESIAN_POINT ( 'NONE',  ( -1.687492729851148177, 28.61614266785989358, 1.663948857909935075 ) ) ;
#3742=VERTEX_POINT ( 'NONE', #1911 ) ;
#3746=AXIS2_PLACEMENT_3D ( 'NONE', #7731, #2737, #5668 ) ;
#3750=DIRECTION ( 'NONE',  ( 0.000000000000000000, 0.000000000000000000, -1.000000000000000000 ) ) ;
#3754=FACE_OUTER_BOUND ( 'NONE', #4787, .T. ) ;
#3756=CARTESIAN_POINT ( 'NONE',  ( 0.000000000000000000, -22.50000000000000355, 2.000000000000013767 ) ) ;
#3776=CARTESIAN_POINT ( 'NONE',  ( 15.00000000000000000, 1.836970198721029589E-15, 26.99999999999999289 ) ) ;
#3777=CARTESIAN_POINT ( 'NONE',  ( 28.75000000000001776, 7.654042494438380704E-16, 1.750000000000019762 ) ) ;
#3797=DIRECTION ( 'NONE',  ( 0.000000000000000000, 0.000000000000000000, -1.000000000000000000 ) ) ;
#3798=CIRCLE ( 'NONE', #2266, 12.50000000000000000 ) ;
#3805=CARTESIAN_POINT ( 'NONE',  ( 0.000000000000000000, 0.000000000000000000, 27.50000000000000355 ) ) ;
#3808=DIRECTION ( 'NONE',  ( -1.000000000000000000, 0.000000000000000000, 0.000000000000000000 ) ) ;
#3813=CIRCLE ( 'NONE', #5973, 3.000000000000000000 ) ;
#3814=CIRCLE ( 'NONE', #1053, 12.50000000000000000 ) ;
#3819=ADVANCED_FACE ( 'NONE', ( #415 ), #6312, .T. ) ;
#3822=VECTOR ( 'NONE', #6836, 1000.000000000000000 ) ;
#3826=FACE_OUTER_BOUND ( 'NONE', #6497, .T. ) ;
#3840=CARTESIAN_POINT ( 'NONE',  ( 6.697288230627575167, -26.42764960499151528, 0.2570604603516986608 ) ) ;
#3841=ORIENTED_EDGE ( 'NONE', *, *, #5540, .T. ) ;
#3842=ORIENTED_EDGE ( 'NONE', *, *, #2964, .F. ) ;
#3850=CARTESIAN_POINT ( 'NONE',  ( -14.49999999999998401, 0.000000000000000000, 27.50000000000000355 ) ) ;
#3858=DIRECTION ( 'NONE',  ( -0.7071067811865486830, 0.000000000000000000, -0.7071067811865464625 ) ) ;
#3865=ORIENTED_EDGE ( 'NONE', *, *, #5990, .F. ) ;
#3875=DIRECTION ( 'NONE',  ( -0.000000000000000000, -0.000000000000000000, -1.000000000000000000 ) ) ;
#3893=ADVANCED_FACE ( 'NONE', ( #7187 ), #6772, .F. ) ;
#3908=DIRECTION ( 'NONE',  ( 1.000000000000000000, 0.000000000000000000, 0.000000000000000000 ) ) ;
#3910=CIRCLE ( 'NONE', #9266, 30.00000000000000000 ) ;
#3912=ORIENTED_EDGE ( 'NONE', *, *, #594, .T. ) ;
#3913=VERTEX_POINT ( 'NONE', #8772 ) ;
#3927=DIRECTION ( 'NONE',  ( -0.000000000000000000, -0.000000000000000000, -1.000000000000000000 ) ) ;
#3931=EDGE_CURVE ( 'NONE', #9459, #3236, #2188, .T. ) ;
#3936=VERTEX_POINT ( 'NONE', #9349 ) ;
#3948=CARTESIAN_POINT ( 'NONE',  ( -26.02777777777775370, 7.180166011355047395, 0.000000000000000000 ) ) ;
#3949=CIRCLE ( 'NONE', #4567, 3.000000000000000000 ) ;
#3951=VERTEX_POINT ( 'NONE', #2733 ) ;
#3952=VECTOR ( 'NONE', #1786, 1000.000000000000000 ) ;
#3954=ORIENTED_EDGE ( 'NONE', *, *, #419, .T. ) ;
#3962=AXIS2_PLACEMENT_3D ( 'NONE', #5776, #6499, #810 ) ;
#3964=CARTESIAN_POINT ( 'NONE',  ( 16.50000000000000000, 0.000000000000000000, 5.000000000000000000 ) ) ;
#3966=ORIENTED_EDGE ( 'NONE', *, *, #540, .T. ) ;
#3981=DIRECTION ( 'NONE',  ( 1.000000000000000000, 0.000000000000000000, 0.000000000000000000 ) ) ;
#4002=ORIENTED_EDGE ( 'NONE', *, *, #8949, .F. ) ;
#4005=DIRECTION ( 'NONE',  ( -0.000000000000000000, -0.000000000000000000, -1.000000000000000000 ) ) ;
#4013=ORIENTED_EDGE ( 'NONE', *, *, #8984, .F. ) ;
#4022=ORIENTED_EDGE ( 'NONE', *, *, #3530, .T. ) ;
#4023=EDGE_LOOP ( 'NONE', ( #4648, #614 ) ) ;
#4026=EDGE_CURVE ( 'NONE', #849, #9116, #2006, .T. ) ;
#4028=DIRECTION ( 'NONE',  ( -0.000000000000000000, -0.000000000000000000, -1.000000000000000000 ) ) ;
#4050=CIRCLE ( 'NONE', #2365, 3.000000000000000000 ) ;
#4055=ORIENTED_EDGE ( 'NONE', *, *, #1713, .F. ) ;
#4063=AXIS2_PLACEMENT_3D ( 'NONE', #4643, #2343, #897 ) ;
#4069=ORIENTED_EDGE ( 'NONE', *, *, #2303, .F. ) ;
#4072=CARTESIAN_POINT ( 'NONE',  ( 16.50000000000000000, 0.000000000000000000, 5.000000000000000000 ) ) ;
#4083=DIRECTION ( 'NONE',  ( 0.000000000000000000, 0.000000000000000000, 1.000000000000000000 ) ) ;
#4084=CYLINDRICAL_SURFACE ( 'NONE', #4976, 6.000000000000000888 ) ;
#4090=EDGE_LOOP ( 'NONE', ( #3157, #4581, #911, #9342 ) ) ;
#4099=CIRCLE ( 'NONE', #7316, 13.50000000000000178 ) ;
#4100=VERTEX_POINT ( 'NONE', #7469 ) ;
#4108=CIRCLE ( 'NONE', #6881, 8.000000000000021316 ) ;
#4121=ORIENTED_EDGE ( 'NONE', *, *, #713, .F. ) ;
#4127=CARTESIAN_POINT ( 'NONE',  ( 28.48725673979378570, 2.337639529181963827, 1.581093618438869086 ) ) ;
#4134=SHAPE_DEFINITION_REPRESENTATION ( #7302, #6298 ) ;
#4136=DIRECTION ( 'NONE',  ( -1.000000000000000000, 0.000000000000000000, 0.000000000000000000 ) ) ;
#4142=EDGE_CURVE ( 'NONE', #3455, #4158, #1854, .T. ) ;
#4146=DIRECTION ( 'NONE',  ( -0.000000000000000000, -0.000000000000000000, -1.000000000000000000 ) ) ;
#4151=EDGE_LOOP ( 'NONE', ( #4393, #5950, #8893, #7944 ) ) ;
#4158=VERTEX_POINT ( 'NONE', #6946 ) ;
#4166=DIRECTION ( 'NONE',  ( 0.000000000000000000, 0.000000000000000000, 1.000000000000000000 ) ) ;
#4170=CARTESIAN_POINT ( 'NONE',  ( 28.61681370049857875, 1.683481704175382010, 1.664380236034806337 ) ) ;
#4181=ORIENTED_EDGE ( 'NONE', *, *, #488, .F. ) ;
#4211=CARTESIAN_POINT ( 'NONE',  ( 28.75000000000003553, 0.3373484206894367676, 1.750000000000026423 ) ) ;
#4214=ORIENTED_EDGE ( 'NONE', *, *, #6950, .T. ) ;
#4219=DIRECTION ( 'NONE',  ( -1.000000000000000000, 0.000000000000000000, 0.000000000000000000 ) ) ;
#4224=ORIENTED_EDGE ( 'NONE', *, *, #6027, .T. ) ;
#4235=EDGE_LOOP ( 'NONE', ( #5851, #7913 ) ) ;
#4244=AXIS2_PLACEMENT_3D ( 'NONE', #6557, #5925, #2989 ) ;
#4246=DIRECTION ( 'NONE',  ( 0.000000000000000000, 0.000000000000000000, 1.000000000000000000 ) ) ;
#4248=CONICAL_SURFACE ( 'NONE', #4563, 14.49999999999998401, 0.7853981633974533860 ) ;
#4251=AXIS2_PLACEMENT_3D ( 'NONE', #715, #3649, #6586 ) ;
#4260=CARTESIAN_POINT ( 'NONE',  ( 14.49999999999998401, 1.775737858763660240E-15, 27.50000000000000355 ) ) ;
#4269=CARTESIAN_POINT ( 'NONE',  ( -25.50000000000000355, 0.000000000000000000, 5.000000000000000000 ) ) ;
#4274=CARTESIAN_POINT ( 'NONE',  ( -22.50000000000000355, 0.000000000000000000, 2.000000000000039080 ) ) ;
#4287=DIRECTION ( 'NONE',  ( -0.2588190451025176309, 0.000000000000000000, -0.9659258262890692004 ) ) ;
#4297=EDGE_CURVE ( 'NONE', #6389, #7685, #2768, .T. ) ;
#4301=CARTESIAN_POINT ( 'NONE',  ( 22.50000000000000355, 0.000000000000000000, 10.00000000000000000 ) ) ;
#4312=VECTOR ( 'NONE', #2856, 1000.000000000000000 ) ;
#4319=EDGE_CURVE ( 'NONE', #3951, #3236, #4776, .T. ) ;
#4320=FACE_OUTER_BOUND ( 'NONE', #8125, .T. ) ;
#4323=CARTESIAN_POINT ( 'NONE',  ( -25.50000000000000355, 0.000000000000000000, 10.00000000000000000 ) ) ;
#4326=ORIENTED_EDGE ( 'NONE', *, *, #6652, .T. ) ;
#4330=CIRCLE ( 'NONE', #5570, 2.999999999999999112 ) ;
#4333=CARTESIAN_POINT ( 'NONE',  ( -28.61681370049858231, -1.683481704175391780, 1.664380236034809890 ) ) ;
#4340=FACE_BOUND ( 'NONE', #4023, .T. ) ;
#4341=ADVANCED_FACE ( 'NONE', ( #2716 ), #4872, .T. ) ;
#4342=CARTESIAN_POINT ( 'NONE',  ( 0.000000000000000000, 22.50000000000000355, 10.00000000000000000 ) ) ;
#4343=DIRECTION ( 'NONE',  ( -1.000000000000000000, 0.000000000000000000, 0.000000000000000000 ) ) ;
#4364=CARTESIAN_POINT ( 'NONE',  ( 0.000000000000000000, -22.50000000000000355, 5.000000000000000000 ) ) ;
#4366=VECTOR ( 'NONE', #6318, 1000.000000000000000 ) ;
#4368=DIRECTION ( 'NONE',  ( 0.000000000000000000, 0.000000000000000000, 1.000000000000000000 ) ) ;
#4378=FACE_OUTER_BOUND ( 'NONE', #5477, .T. ) ;
#4388=CIRCLE ( 'NONE', #8988, 15.00000000000000000 ) ;
#4393=ORIENTED_EDGE ( 'NONE', *, *, #7358, .F. ) ;
#4399=FACE_OUTER_BOUND ( 'NONE', #6735, .T. ) ;
#4404=VERTEX_POINT ( 'NONE', #1993 ) ;
#4422=VERTEX_POINT ( 'NONE', #5016 ) ;
#4429=FACE_OUTER_BOUND ( 'NONE', #4090, .T. ) ;
#4431=DIRECTION ( 'NONE',  ( -1.000000000000000000, 0.000000000000000000, -0.000000000000000000 ) ) ;
#4437=DIRECTION ( 'NONE',  ( -1.000000000000000000, 0.000000000000000000, 0.000000000000000000 ) ) ;
#4449=DIRECTION ( 'NONE',  ( 0.7071067811865479058, 0.000000000000000000, 0.7071067811865471286 ) ) ;
#4450=DIRECTION ( 'NONE',  ( -0.000000000000000000, -0.000000000000000000, -1.000000000000000000 ) ) ;
#4451=CARTESIAN_POINT ( 'NONE',  ( 12.50000000000000000, 1.530808498934191127E-15, 28.50000000000000355 ) ) ;
#4454=DIRECTION ( 'NONE',  ( -1.000000000000000000, 0.000000000000000000, 0.000000000000000000 ) ) ;
#4457=ORIENTED_EDGE ( 'NONE', *, *, #6649, .F. ) ;
#4462=CARTESIAN_POINT ( 'NONE',  ( -0.6837532375831764098, 28.73276100836656610, 1.738917791092793319 ) ) ;
#4469=CARTESIAN_POINT ( 'NONE',  ( 0.000000000000000000, 0.000000000000000000, 2.999999999999999112 ) ) ;
#4470=CYLINDRICAL_SURFACE ( 'NONE', #7965, 6.000000000000001776 ) ;
#4484=ORIENTED_EDGE ( 'NONE', *, *, #709, .T. ) ;
#4487=DIRECTION ( 'NONE',  ( 1.000000000000000000, 0.000000000000000000, 0.000000000000000000 ) ) ;
#4492=CARTESIAN_POINT ( 'NONE',  ( -11.96410161513786008, 0.000000000000000000, 50.00000000000000000 ) ) ;
#4499=VERTEX_POINT ( 'NONE', #6608 ) ;
#4500=CIRCLE ( 'NONE', #1583, 6.000000000000000888 ) ;
#4501=DIRECTION ( 'NONE',  ( -1.000000000000000000, 0.000000000000000000, 0.000000000000000000 ) ) ;
#4504=CARTESIAN_POINT ( 'NONE',  ( 7.180166011355011868, 26.02777777777776791, 0.000000000000000000 ) ) ;
#4507=CARTESIAN_POINT ( 'NONE',  ( 15.00000000000000000, 1.836970198721029589E-15, 10.00000000000000000 ) ) ;
#4536=VERTEX_POINT ( 'NONE', #6695 ) ;
#4539=DIRECTION ( 'NONE',  ( 1.000000000000000000, 0.000000000000000000, 0.000000000000000000 ) ) ;
#4545=AXIS2_PLACEMENT_3D ( 'NONE', #5866, #5091, #767 ) ;
#4546=VECTOR ( 'NONE', #9018, 1000.000000000000000 ) ;
#4559=CARTESIAN_POINT ( 'NONE',  ( -5.103771271004210242, 27.45068023253072909, 0.9147230066269097515 ) ) ;
#4562=CARTESIAN_POINT ( 'NONE',  ( 2.341162148116626263, -28.48643429264087246, 1.580564902411995210 ) ) ;
#4563=AXIS2_PLACEMENT_3D ( 'NONE', #1642, #5248, #8174 ) ;
#4564=EDGE_LOOP ( 'NONE', ( #2974, #6838 ) ) ;
#4567=AXIS2_PLACEMENT_3D ( 'NONE', #4364, #3736, #4501 ) ;
#4581=ORIENTED_EDGE ( 'NONE', *, *, #1288, .T. ) ;
#4588=ORIENTED_EDGE ( 'NONE', *, *, #7882, .F. ) ;
#4601=CARTESIAN_POINT ( 'NONE',  ( 0.000000000000000000, -22.50000000000000355, 5.000000000000000000 ) ) ;
#4606=CARTESIAN_POINT ( 'NONE',  ( 0.000000000000000000, 0.000000000000000000, 0.000000000000000000 ) ) ;
#4607=CARTESIAN_POINT ( 'NONE',  ( 0.000000000000000000, -22.50000000000000355, 2.000000000000013767 ) ) ;
#4613=ORIENTED_EDGE ( 'NONE', *, *, #1236, .T. ) ;
#4614=CYLINDRICAL_SURFACE ( 'NONE', #5001, 6.000000000000000888 ) ;
#4622=AXIS2_PLACEMENT_3D ( 'NONE', #7081, #544, #4343 ) ;
#4638=ORIENTED_EDGE ( 'NONE', *, *, #2647, .F. ) ;
#4641=DIRECTION ( 'NONE',  ( -0.000000000000000000, -0.000000000000000000, 1.000000000000000000 ) ) ;
#4643=CARTESIAN_POINT ( 'NONE',  ( 0.000000000000000000, 0.000000000000000000, 27.50000000000000355 ) ) ;
#4646=FACE_OUTER_BOUND ( 'NONE', #6301, .T. ) ;
#4648=ORIENTED_EDGE ( 'NONE', *, *, #7399, .F. ) ;
#4651=CARTESIAN_POINT ( 'NONE',  ( 15.00000000000000000, 1.836970198721029589E-15, 27.50000000000000355 ) ) ;
#4657=ADVANCED_FACE ( 'NONE', ( #3278 ), #6984, .F. ) ;
#4666=FACE_OUTER_BOUND ( 'NONE', #7437, .T. ) ;
#4669=LINE ( 'NONE', #9172, #3822 ) ;
#4677=LINE ( 'NONE', #1695, #650 ) ;
#4678=CIRCLE ( 'NONE', #2833, 6.000000000000000888 ) ;
#4689=DIRECTION ( 'NONE',  ( -0.000000000000000000, -0.000000000000000000, -1.000000000000000000 ) ) ;
#4693=DIRECTION ( 'NONE',  ( 0.000000000000000000, 0.000000000000000000, -1.000000000000000000 ) ) ;
#4704=DIRECTION ( 'NONE',  ( -1.000000000000000000, 0.000000000000000000, 0.000000000000000000 ) ) ;
#4717=DIRECTION ( 'NONE',  ( 0.000000000000000000, 0.000000000000000000, -1.000000000000000000 ) ) ;
#4719=AXIS2_PLACEMENT_3D ( 'NONE', #3692, #4368, #5046 ) ;
#4743=CARTESIAN_POINT ( 'NONE',  ( -12.50000000000000000, 0.000000000000000000, 50.00000000000000000 ) ) ;
#4749=FACE_BOUND ( 'NONE', #5079, .T. ) ;
#4751=ORIENTED_EDGE ( 'NONE', *, *, #709, .F. ) ;
#4753=CARTESIAN_POINT ( 'NONE',  ( 0.000000000000000000, 0.000000000000000000, 50.00000000000000000 ) ) ;
#4758=ORIENTED_EDGE ( 'NONE', *, *, #1831, .T. ) ;
#4762=DIRECTION ( 'NONE',  ( -1.000000000000000000, 0.000000000000000000, 0.000000000000000000 ) ) ;
#4767=ORIENTED_EDGE ( 'NONE', *, *, #3931, .F. ) ;
#4768=DIRECTION ( 'NONE',  ( -0.000000000000000000, -0.000000000000000000, -1.000000000000000000 ) ) ;
#4776=CIRCLE ( 'NONE', #177, 3.000000000000000000 ) ;
#4785=CARTESIAN_POINT ( 'NONE',  ( 6.000000000000000888, -22.50000000000000355, 2.000000000000013767 ) ) ;
#4787=EDGE_LOOP ( 'NONE', ( #4457, #8965, #5052, #3405 ) ) ;
#4794=CARTESIAN_POINT ( 'NONE',  ( 0.000000000000000000, 0.000000000000000000, 28.50000000000000355 ) ) ;
#4795=VECTOR ( 'NONE', #8034, 1000.000000000000000 ) ;
#4798=ORIENTED_EDGE ( 'NONE', *, *, #2303, .T. ) ;
#4802=CARTESIAN_POINT ( 'NONE',  ( 0.000000000000000000, 0.000000000000000000, 2.999999999999999112 ) ) ;
#4805=VECTOR ( 'NONE', #3551, 1000.000000000000000 ) ;
#4812=EDGE_CURVE ( 'NONE', #2492, #3951, #7931, .T. ) ;
#4813=DIRECTION ( 'NONE',  ( -1.000000000000000000, 0.000000000000000000, 0.000000000000000000 ) ) ;
#4817=ORIENTED_EDGE ( 'NONE', *, *, #5890, .F. ) ;
#4822=DIRECTION ( 'NONE',  ( 1.000000000000000000, 0.000000000000000000, 0.000000000000000000 ) ) ;
#4823=EDGE_CURVE ( 'NONE', #7976, #4945, #3814, .T. ) ;
#4827=AXIS2_PLACEMENT_3D ( 'NONE', #2176, #4246, #7176 ) ;
#4830=EDGE_CURVE ( 'NONE', #7998, #7322, #8603, .T. ) ;
#4832=ORIENTED_EDGE ( 'NONE', *, *, #1717, .T. ) ;
#4834=PLANE ( 'NONE',  #5305 ) ;
#4845=CARTESIAN_POINT ( 'NONE',  ( 26.02777777777776791, 7.180166011355005651, 0.000000000000000000 ) ) ;
#4857=EDGE_LOOP ( 'NONE', ( #8209, #1605, #1423, #4767 ) ) ;
#4866=VERTEX_POINT ( 'NONE', #2316 ) ;
#4872=CYLINDRICAL_SURFACE ( 'NONE', #4622, 15.00000000000000000 ) ;
#4874=CIRCLE ( 'NONE', #6123, 6.000000000000000888 ) ;
#4884=LINE ( 'NONE', #4260, #7484 ) ;
#4885=AXIS2_PLACEMENT_3D ( 'NONE', #5854, #9474, #5999 ) ;
#4891=CARTESIAN_POINT ( 'NONE',  ( -6.702350214711367826, -26.42345776824586423, 0.2543657081580636414 ) ) ;
#4900=DIRECTION ( 'NONE',  ( 1.000000000000000000, 0.000000000000000000, 0.000000000000000000 ) ) ;
#4904=ORIENTED_EDGE ( 'NONE', *, *, #145, .F. ) ;
#4920=ADVANCED_FACE ( 'NONE', ( #5195 ), #4470, .F. ) ;
#4938=EDGE_CURVE ( 'NONE', #5908, #386, #3497, .T. ) ;
#4941=DIRECTION ( 'NONE',  ( -0.000000000000000000, -0.000000000000000000, -1.000000000000000000 ) ) ;
#4945=VERTEX_POINT ( 'NONE', #8747 ) ;
#4954=CIRCLE ( 'NONE', #972, 2.999999999999999112 ) ;
#4972=CARTESIAN_POINT ( 'NONE',  ( -7.180166011355011868, 26.02777777777776436, 0.000000000000000000 ) ) ;
#4976=AXIS2_PLACEMENT_3D ( 'NONE', #571, #3363, #6306 ) ;
#4981=VECTOR ( 'NONE', #3031, 1000.000000000000000 ) ;
#4990=MANIFOLD_SOLID_BREP ( 'Pah5', #3635 ) ;
#4993=ORIENTED_EDGE ( 'NONE', *, *, #3426, .T. ) ;
#4996=ADVANCED_FACE ( 'NONE', ( #4429 ), #838, .F. ) ;
#4998=EDGE_CURVE ( 'NONE', #1940, #3913, #769, .T. ) ;
#5001=AXIS2_PLACEMENT_3D ( 'NONE', #3078, #8931, #3124 ) ;
#5016=CARTESIAN_POINT ( 'NONE',  ( -14.49999999999998401, 0.000000000000000000, 27.50000000000000355 ) ) ;
#5032=CARTESIAN_POINT ( 'NONE',  ( 0.000000000000000000, -22.50000000000000355, 2.000000000000013767 ) ) ;
#5036=DIRECTION ( 'NONE',  ( 0.000000000000000000, 0.000000000000000000, -1.000000000000000000 ) ) ;
#5042=ADVANCED_FACE ( 'NONE', ( #6066, #382 ), #2606, .T. ) ;
#5044=VECTOR ( 'NONE', #4287, 1000.000000000000000 ) ;
#5046=DIRECTION ( 'NONE',  ( 1.000000000000000000, 0.000000000000000000, 0.000000000000000000 ) ) ;
#5052=ORIENTED_EDGE ( 'NONE', *, *, #6254, .T. ) ;
#5069=CARTESIAN_POINT ( 'NONE',  ( 0.000000000000000000, 22.50000000000000355, 0.000000000000000000 ) ) ;
#5079=EDGE_LOOP ( 'NONE', ( #8145, #6578 ) ) ;
#5091=DIRECTION ( 'NONE',  ( 0.000000000000000000, 0.000000000000000000, -1.000000000000000000 ) ) ;
#5092=AXIS2_PLACEMENT_3D ( 'NONE', #6743, #8079, #7445 ) ;
#5094=CARTESIAN_POINT ( 'NONE',  ( 22.50000000000000355, 0.000000000000000000, 5.000000000000000000 ) ) ;
#5101=EDGE_LOOP ( 'NONE', ( #8744, #4069, #7620, #8294 ) ) ;
#5107=DIRECTION ( 'NONE',  ( -1.000000000000000000, 0.000000000000000000, 0.000000000000000000 ) ) ;
#5136=ORIENTED_EDGE ( 'NONE', *, *, #1293, .F. ) ;
#5144=CYLINDRICAL_SURFACE ( 'NONE', #8026, 2.999999999999999112 ) ;
#5147=DIRECTION ( 'NONE',  ( 0.000000000000000000, 0.000000000000000000, -1.000000000000000000 ) ) ;
#5149=CYLINDRICAL_SURFACE ( 'NONE', #1952, 12.50000000000000000 ) ;
#5152=CARTESIAN_POINT ( 'NONE',  ( -22.50000000000000355, 0.000000000000000000, 5.000000000000000000 ) ) ;
#5158=EDGE_LOOP ( 'NONE', ( #2182, #7260, #6816, #7319 ) ) ;
#5172=CARTESIAN_POINT ( 'NONE',  ( 0.000000000000000000, 0.000000000000000000, 48.00000000000036948 ) ) ;
#5180=CARTESIAN_POINT ( 'NONE',  ( -0.3423334138323023135, 28.74982858564768762, 1.749889805059230419 ) ) ;
#5181=AXIS2_PLACEMENT_3D ( 'NONE', #3220, #6783, #6741 ) ;
#5192=CARTESIAN_POINT ( 'NONE',  ( -22.50000000000000355, 0.000000000000000000, 10.00000000000000000 ) ) ;
#5193=VECTOR ( 'NONE', #5688, 1000.000000000000000 ) ;
#5194=B_SPLINE_CURVE_WITH_KNOTS ( 'NONE', 3,
 ( #3777, #6146, #1805, #8387, #6719, #2346, #5994, #9058, #6859, #2393, #9011, #6042, #2532, #8962 ),
 .UNSPECIFIED., .F., .F.,
 ( 4, 2, 2, 2, 2, 2, 4 ),
 ( 0.008014353914675810889, 0.01001537843003028581, 0.01101589068770752328, 0.01201640294538476247, 0.01301691520306200167, 0.01401742746073924087, 0.01601845197609371926 ),
 .UNSPECIFIED. ) ;
#5195=FACE_OUTER_BOUND ( 'NONE', #2812, .T. ) ;
#5196=CARTESIAN_POINT ( 'NONE',  ( 26.02777777777776436, -7.180166011355007427, 0.000000000000000000 ) ) ;
#5211=( LENGTH_UNIT ( ) NAMED_UNIT ( * ) SI_UNIT ( .MILLI., .METRE. ) );
#5213=EDGE_CURVE ( 'NONE', #5549, #9261, #3910, .T. ) ;
#5219=EDGE_CURVE ( 'NONE', #3742, #662, #994, .T. ) ;
#5229=CARTESIAN_POINT ( 'NONE',  ( 3.288881746422226193, 28.22045692612880075, 1.409579452511374065 ) ) ;
#5234=ORIENTED_EDGE ( 'NONE', *, *, #3359, .T. ) ;
#5241=ADVANCED_FACE ( 'NONE', ( #8050 ), #3682, .F. ) ;
#5245=DIRECTION ( 'NONE',  ( -1.000000000000000000, 0.000000000000000000, 0.000000000000000000 ) ) ;
#5248=DIRECTION ( 'NONE',  ( 0.000000000000000000, 0.000000000000000000, -1.000000000000000000 ) ) ;
#5254=PLANE ( 'NONE',  #9389 ) ;
#5256=ADVANCED_FACE ( 'NONE', ( #4399 ), #2190, .F. ) ;
#5258=ADVANCED_FACE ( 'NONE', ( #7148 ), #4084, .F. ) ;
#5264=EDGE_LOOP ( 'NONE', ( #6351, #5454, #3343, #6399, #449, #9091 ) ) ;
#5270=DIRECTION ( 'NONE',  ( -1.000000000000000000, 0.000000000000000000, 0.000000000000000000 ) ) ;
#5279=ORIENTED_EDGE ( 'NONE', *, *, #8541, .T. ) ;
#5282=AXIS2_PLACEMENT_3D ( 'NONE', #3648, #8924, #9452 ) ;
#5305=AXIS2_PLACEMENT_3D ( 'NONE', #7813, #1222, #7087 ) ;
#5317=CARTESIAN_POINT ( 'NONE',  ( 22.50000000000000355, 0.000000000000000000, 0.000000000000000000 ) ) ;
#5326=ORIENTED_EDGE ( 'NONE', *, *, #4812, .F. ) ;
#5327=VECTOR ( 'NONE', #4689, 1000.000000000000000 ) ;
#5328=CARTESIAN_POINT ( 'NONE',  ( 0.000000000000000000, 0.000000000000000000, 10.00000000000000000 ) ) ;
#5331=VERTEX_POINT ( 'NONE', #2291 ) ;
#5336=DIRECTION ( 'NONE',  ( 0.000000000000000000, 0.000000000000000000, 1.000000000000000000 ) ) ;
#5351=CARTESIAN_POINT ( 'NONE',  ( -28.40858913551337750, 2.655051044735472487, 1.530521587115753812 ) ) ;
#5379=CARTESIAN_POINT ( 'NONE',  ( 0.000000000000000000, 22.50000000000000355, 10.00000000000000000 ) ) ;
#5380=VERTEX_POINT ( 'NONE', #226 ) ;
#5384=CARTESIAN_POINT ( 'NONE',  ( 5.088821267330767562, 27.44505377838575200, 0.9111060003908462157 ) ) ;
#5385=DIRECTION ( 'NONE',  ( 0.000000000000000000, 0.000000000000000000, -1.000000000000000000 ) ) ;
#5386=CARTESIAN_POINT ( 'NONE',  ( -3.288881746422226193, -28.22045692612880075, 1.409579452511374065 ) ) ;
#5387=EDGE_LOOP ( 'NONE', ( #3075, #5518, #7065, #7726, #9147, #541, #9227, #6811 ) ) ;
#5394=DIRECTION ( 'NONE',  ( 0.7071067811865439090, 8.659560562354888485E-17, -0.7071067811865511255 ) ) ;
#5395=DIRECTION ( 'NONE',  ( 1.000000000000000000, 0.000000000000000000, 0.000000000000000000 ) ) ;
#5398=ORIENTED_EDGE ( 'NONE', *, *, #6218, .T. ) ;
#5404=AXIS2_PLACEMENT_3D ( 'NONE', #6609, #393, #3908 ) ;
#5419=VERTEX_POINT ( 'NONE', #940 ) ;
#5428=CYLINDRICAL_SURFACE ( 'NONE', #7581, 30.00000000000000000 ) ;
#5429=CARTESIAN_POINT ( 'NONE',  ( -3.600085285568724203, -28.11218154377481682, 1.339973849569531472 ) ) ;
#5435=ADVANCED_FACE ( 'NONE', ( #5939 ), #236, .T. ) ;
#5442=ORIENTED_EDGE ( 'NONE', *, *, #308, .T. ) ;
#5445=ORIENTED_EDGE ( 'NONE', *, *, #4142, .F. ) ;
#5454=ORIENTED_EDGE ( 'NONE', *, *, #6266, .F. ) ;
#5465=VERTEX_POINT ( 'NONE', #3061 ) ;
#5469=FACE_OUTER_BOUND ( 'NONE', #86, .T. ) ;
#5472=CIRCLE ( 'NONE', #4545, 6.000000000000000888 ) ;
#5474=FACE_OUTER_BOUND ( 'NONE', #5387, .T. ) ;
#5475=DIRECTION ( 'NONE',  ( 0.000000000000000000, 0.000000000000000000, -1.000000000000000000 ) ) ;
#5477=EDGE_LOOP ( 'NONE', ( #3841, #3249 ) ) ;
#5487=AXIS2_PLACEMENT_3D ( 'NONE', #3260, #5475, #8349 ) ;
#5490=EDGE_LOOP ( 'NONE', ( #6010, #6122, #5729, #6493 ) ) ;
#5494=AXIS2_PLACEMENT_3D ( 'NONE', #7244, #3592, #6529 ) ;
#5495=CARTESIAN_POINT ( 'NONE',  ( -22.50000000000000355, 0.000000000000000000, 5.000000000000000000 ) ) ;
#5504=DIRECTION ( 'NONE',  ( 0.000000000000000000, 0.000000000000000000, 1.000000000000000000 ) ) ;
#5518=ORIENTED_EDGE ( 'NONE', *, *, #3163, .T. ) ;
#5534=CARTESIAN_POINT ( 'NONE',  ( -27.28672223502583449, 5.374373886926214539, 0.8093214368023373684 ) ) ;
#5537=CARTESIAN_POINT ( 'NONE',  ( 25.50000000000000355, 3.673940397442056417E-16, 10.00000000000000000 ) ) ;
#5539=VERTEX_POINT ( 'NONE', #6188 ) ;
#5540=EDGE_CURVE ( 'NONE', #9435, #5792, #4678, .T. ) ;
#5541=CARTESIAN_POINT ( 'NONE',  ( 0.000000000000000000, 0.000000000000000000, 50.00000000000000000 ) ) ;
#5548=LINE ( 'NONE', #7569, #724 ) ;
#5549=VERTEX_POINT ( 'NONE', #1946 ) ;
#5552=ORIENTED_EDGE ( 'NONE', *, *, #6254, .F. ) ;
#5569=ORIENTED_EDGE ( 'NONE', *, *, #1889, .F. ) ;
#5570=AXIS2_PLACEMENT_3D ( 'NONE', #6640, #8889, #1541 ) ;
#5577=VERTEX_POINT ( 'NONE', #4785 ) ;
#5584=ORIENTED_EDGE ( 'NONE', *, *, #3139, .T. ) ;
#5624=DIRECTION ( 'NONE',  ( -0.000000000000000000, -0.000000000000000000, 1.000000000000000000 ) ) ;
#5638=CARTESIAN_POINT ( 'NONE',  ( 0.000000000000000000, 0.000000000000000000, 28.50000000000000355 ) ) ;
#5647=CIRCLE ( 'NONE', #6716, 26.99999999999999645 ) ;
#5648=DIRECTION ( 'NONE',  ( 0.000000000000000000, 0.000000000000000000, -1.000000000000000000 ) ) ;
#5656=ORIENTED_EDGE ( 'NONE', *, *, #4026, .F. ) ;
#5661=EDGE_CURVE ( 'NONE', #450, #1766, #5758, .T. ) ;
#5668=DIRECTION ( 'NONE',  ( -1.000000000000000000, 0.000000000000000000, 0.000000000000000000 ) ) ;
#5669=VECTOR ( 'NONE', #7903, 1000.000000000000000 ) ;
#5670=CARTESIAN_POINT ( 'NONE',  ( 26.79453276911118564, 6.186305604711932027, 0.4929139230000564864 ) ) ;
#5671=EDGE_LOOP ( 'NONE', ( #637, #8350, #1602, #4022 ) ) ;
#5675=EDGE_CURVE ( 'NONE', #5465, #4422, #6982, .T. ) ;
#5688=DIRECTION ( 'NONE',  ( -0.000000000000000000, -0.000000000000000000, -1.000000000000000000 ) ) ;
#5698=VECTOR ( 'NONE', #983, 1000.000000000000000 ) ;
#5705=ORIENTED_EDGE ( 'NONE', *, *, #6878, .T. ) ;
#5715=ORIENTED_EDGE ( 'NONE', *, *, #2371, .T. ) ;
#5723=CARTESIAN_POINT ( 'NONE',  ( 6.000000000000000888, -22.50000000000000355, 5.000000000000000000 ) ) ;
#5725=ORIENTED_EDGE ( 'NONE', *, *, #8833, .F. ) ;
#5727=CIRCLE ( 'NONE', #9084, 15.00000000000000000 ) ;
#5729=ORIENTED_EDGE ( 'NONE', *, *, #4998, .T. ) ;
#5735=AXIS2_PLACEMENT_3D ( 'NONE', #7974, #3448, #4136 ) ;
#5749=EDGE_LOOP ( 'NONE', ( #8832, #4588 ) ) ;
#5756=CARTESIAN_POINT ( 'NONE',  ( 0.000000000000000000, 22.50000000000000355, 2.000000000000013767 ) ) ;
#5758=CIRCLE ( 'NONE', #1603, 2.999999999999999112 ) ;
#5776=CARTESIAN_POINT ( 'NONE',  ( 0.000000000000000000, 22.50000000000000355, 2.000000000000013767 ) ) ;
#5784=CARTESIAN_POINT ( 'NONE',  ( 0.000000000000000000, 0.000000000000000000, 50.00000000000000000 ) ) ;
#5790=AXIS2_PLACEMENT_3D ( 'NONE', #2215, #5147, #8841 ) ;
#5792=VERTEX_POINT ( 'NONE', #8992 ) ;
#5796=AXIS2_PLACEMENT_3D ( 'NONE', #4469, #2314, #8170 ) ;
#5812=VERTEX_POINT ( 'NONE', #118 ) ;
#5844=EDGE_CURVE ( 'NONE', #4499, #3178, #1722, .T. ) ;
#5847=DIRECTION ( 'NONE',  ( 1.000000000000000000, 0.000000000000000000, 0.000000000000000000 ) ) ;
#5851=ORIENTED_EDGE ( 'NONE', *, *, #8363, .T. ) ;
#5854=CARTESIAN_POINT ( 'NONE',  ( -22.50000000000000355, 0.000000000000000000, 2.000000000000039080 ) ) ;
#5866=CARTESIAN_POINT ( 'NONE',  ( 0.000000000000000000, 22.50000000000000355, 5.000000000000000000 ) ) ;
#5877=AXIS2_PLACEMENT_3D ( 'NONE', #9137, #6038, #315 ) ;
#5879=B_SPLINE_CURVE_WITH_KNOTS ( 'NONE', 3,
 ( #799, #8115, #851, #4559, #6727, #2247, #2354, #6626, #6819, #3738, #5902, #4462, #5180, #8261, #6053, #1575, #1624, #5229, #1723, #8163, #6675, #5384, #7482, #8826, #90, #4504 ),
 .UNSPECIFIED., .F., .F.,
 ( 4, 2, 2, 2, 2, 2, 2, 2, 2, 2, 2, 2, 4 ),
 ( 1.812491582141323212E-18, 0.002002306497011713607, 0.004004612994023425479, 0.005005766242529281415, 0.006006919491035139086, 0.007008072739540995022, 0.008009225988046852693, 0.01001153248505856456, 0.01101268573356442224, 0.01201383898207027817, 0.01301499223057613411, 0.01401614547908198831, 0.01601845197609370539 ),
 .UNSPECIFIED. ) ;
#5884=CIRCLE ( 'NONE', #8948, 6.000000000000001776 ) ;
#5885=ORIENTED_EDGE ( 'NONE', *, *, #4938, .T. ) ;
#5886=( NAMED_UNIT ( * ) SI_UNIT ( $, .STERADIAN. ) SOLID_ANGLE_UNIT ( ) );
#5890=EDGE_CURVE ( 'NONE', #7651, #933, #8004, .T. ) ;
#5902=CARTESIAN_POINT ( 'NONE',  ( -1.356121383298963590, 28.66577847273270763, 1.695857589613878558 ) ) ;
#5908=VERTEX_POINT ( 'NONE', #3964 ) ;
#5922=CIRCLE ( 'NONE', #9282, 30.00000000000000000 ) ;
#5925=DIRECTION ( 'NONE',  ( -0.000000000000000000, -0.000000000000000000, -1.000000000000000000 ) ) ;
#5939=FACE_OUTER_BOUND ( 'NONE', #197, .T. ) ;
#5943=CIRCLE ( 'NONE', #5796, 30.00000000000000000 ) ;
#5950=ORIENTED_EDGE ( 'NONE', *, *, #1889, .T. ) ;
#5957=DIRECTION ( 'NONE',  ( -0.000000000000000000, -0.000000000000000000, -1.000000000000000000 ) ) ;
#5973=AXIS2_PLACEMENT_3D ( 'NONE', #2728, #6381, #7959 ) ;
#5984=ORIENTED_EDGE ( 'NONE', *, *, #549, .T. ) ;
#5986=ORIENTED_EDGE ( 'NONE', *, *, #8833, .T. ) ;
#5990=EDGE_CURVE ( 'NONE', #3178, #4404, #6630, .T. ) ;
#5994=CARTESIAN_POINT ( 'NONE',  ( 28.11123945536280644, -3.602653646940633614, 1.339368221304666262 ) ) ;
#5999=DIRECTION ( 'NONE',  ( -1.000000000000000000, 0.000000000000000000, 0.000000000000000000 ) ) ;
#6008=FACE_OUTER_BOUND ( 'NONE', #8682, .T. ) ;
#6010=ORIENTED_EDGE ( 'NONE', *, *, #1190, .F. ) ;
#6018=DIRECTION ( 'NONE',  ( -0.7071067811865439090, 0.000000000000000000, -0.7071067811865511255 ) ) ;
#6019=CARTESIAN_POINT ( 'NONE',  ( 0.000000000000000000, 0.000000000000000000, 27.50000000000000355 ) ) ;
#6021=ADVANCED_FACE ( 'NONE', ( #533 ), #6457, .T. ) ;
#6027=EDGE_CURVE ( 'NONE', #7651, #651, #7431, .T. ) ;
#6028=AXIS2_PLACEMENT_3D ( 'NONE', #5541, #1108, #2755 ) ;
#6030=DIRECTION ( 'NONE',  ( 1.000000000000000000, 0.000000000000000000, 0.000000000000000000 ) ) ;
#6033=ORIENTED_EDGE ( 'NONE', *, *, #2964, .T. ) ;
#6034=( NAMED_UNIT ( * ) SI_UNIT ( $, .STERADIAN. ) SOLID_ANGLE_UNIT ( ) );
#6038=DIRECTION ( 'NONE',  ( 0.000000000000000000, 0.000000000000000000, -1.000000000000000000 ) ) ;
#6040=DIRECTION ( 'NONE',  ( 0.000000000000000000, 0.000000000000000000, 1.000000000000000000 ) ) ;
#6042=CARTESIAN_POINT ( 'NONE',  ( 26.78965207131484050, -6.193975265304529465, 0.4897763315595429767 ) ) ;
#6048=FACE_BOUND ( 'NONE', #2534, .T. ) ;
#6053=CARTESIAN_POINT ( 'NONE',  ( 1.335553917663280021, 28.68463450227767453, 1.707979322892793306 ) ) ;
#6066=FACE_BOUND ( 'NONE', #4564, .T. ) ;
#6071=CARTESIAN_POINT ( 'NONE',  ( 0.000000000000000000, 0.000000000000000000, 26.99999999999999289 ) ) ;
#6078=STYLED_ITEM('',(#9529),#4990);
#6085=ORIENTED_EDGE ( 'NONE', *, *, #7638, .F. ) ;
#6087=CARTESIAN_POINT ( 'NONE',  ( 0.000000000000000000, 22.50000000000000355, 0.000000000000000000 ) ) ;
#6098=CONICAL_SURFACE ( 'NONE', #8686, 6.000000000000001776, 0.7853981633974500554 ) ;
#6108=CIRCLE ( 'NONE', #5790, 2.999999999999999112 ) ;
#6113=AXIS2_PLACEMENT_3D ( 'NONE', #2930, #6682, #3029 ) ;
#6121=DIRECTION ( 'NONE',  ( 0.000000000000000000, 0.000000000000000000, -1.000000000000000000 ) ) ;
#6122=ORIENTED_EDGE ( 'NONE', *, *, #7110, .F. ) ;
#6123=AXIS2_PLACEMENT_3D ( 'NONE', #5756, #464, #606 ) ;
#6136=VERTEX_POINT ( 'NONE', #5196 ) ;
#6138=SHAPE_REPRESENTATION_RELATIONSHIP ( 'NONE' , 'NONE' ,  #6298, #8060 ) ;
#6146=CARTESIAN_POINT ( 'NONE',  ( 28.75000000000002842, -0.6738334415499637187, 1.750000000000026423 ) ) ;
#6158=CARTESIAN_POINT ( 'NONE',  ( 1.687492729851148177, -28.61614266785989358, 1.663948857909935075 ) ) ;
#6167=CARTESIAN_POINT ( 'NONE',  ( -28.21952111405550312, 3.291689805591859752, 1.408977859035693170 ) ) ;
#6168=EDGE_CURVE ( 'NONE', #3913, #5419, #7707, .T. ) ;
#6185=DIRECTION ( 'NONE',  ( 0.000000000000000000, 0.000000000000000000, 1.000000000000000000 ) ) ;
#6188=CARTESIAN_POINT ( 'NONE',  ( 3.000000000000000000, -22.50000000000000355, 10.00000000000000000 ) ) ;
#6191=VERTEX_POINT ( 'NONE', #8937 ) ;
#6202=CARTESIAN_POINT ( 'NONE',  ( 0.000000000000000000, 0.000000000000000000, 10.00000000000000000 ) ) ;
#6218=EDGE_CURVE ( 'NONE', #5331, #3688, #4330, .T. ) ;
#6233=DIRECTION ( 'NONE',  ( 0.000000000000000000, 0.000000000000000000, -1.000000000000000000 ) ) ;
#6244=AXIS2_PLACEMENT_3D ( 'NONE', #5328, #6913, #9151 ) ;
#6254=EDGE_CURVE ( 'NONE', #4422, #7550, #8748, .T. ) ;
#6262=CARTESIAN_POINT ( 'NONE',  ( 28.50000000000000355, 7.347880794884122694E-16, 2.000000000000035083 ) ) ;
#6266=EDGE_CURVE ( 'NONE', #6389, #8082, #3101, .T. ) ;
#6275=AXIS2_PLACEMENT_3D ( 'NONE', #1725, #5336, #241 ) ;
#6284=CARTESIAN_POINT ( 'NONE',  ( 30.00000000000000000, 3.673940397442059178E-15, 10.00000000000000000 ) ) ;
#6292=ORIENTED_EDGE ( 'NONE', *, *, #5844, .T. ) ;
#6296=CARTESIAN_POINT ( 'NONE',  ( -8.000000000000021316, 22.50000000000000355, 0.000000000000000000 ) ) ;
#6298=SHAPE_REPRESENTATION ( '4-Axle(Cross)', ( #1614 ), #1322 ) ;
#6300=DIRECTION ( 'NONE',  ( -1.000000000000000000, 0.000000000000000000, 0.000000000000000000 ) ) ;
#6301=EDGE_LOOP ( 'NONE', ( #5326, #8722, #8975, #237 ) ) ;
#6306=DIRECTION ( 'NONE',  ( -1.000000000000000000, 0.000000000000000000, 0.000000000000000000 ) ) ;
#6311=ORIENTED_EDGE ( 'NONE', *, *, #7358, .T. ) ;
#6312=CONICAL_SURFACE ( 'NONE', #8899, 11.96410161513786008, 0.2617993877991461882 ) ;
#6318=DIRECTION ( 'NONE',  ( -0.7071067811865479058, 8.659560562354937789E-17, 0.7071067811865471286 ) ) ;
#6328=DIRECTION ( 'NONE',  ( -1.000000000000000000, 0.000000000000000000, 0.000000000000000000 ) ) ;
#6339=DIRECTION ( 'NONE',  ( 1.000000000000000000, 0.000000000000000000, 0.000000000000000000 ) ) ;
#6340=ORIENTED_EDGE ( 'NONE', *, *, #194, .T. ) ;
#6351=ORIENTED_EDGE ( 'NONE', *, *, #1288, .F. ) ;
#6359=ADVANCED_FACE ( 'NONE', ( #3641 ), #6730, .F. ) ;
#6371=DIRECTION ( 'NONE',  ( 0.000000000000000000, 0.000000000000000000, -1.000000000000000000 ) ) ;
#6372=AXIS2_PLACEMENT_3D ( 'NONE', #1972, #4941, #8549 ) ;
#6378=ORIENTED_EDGE ( 'NONE', *, *, #8231, .T. ) ;
#6381=DIRECTION ( 'NONE',  ( 0.000000000000000000, 0.000000000000000000, -1.000000000000000000 ) ) ;
#6387=CARTESIAN_POINT ( 'NONE',  ( -6.193323906411744240, -26.79012200670185351, 0.4900784328797758715 ) ) ;
#6389=VERTEX_POINT ( 'NONE', #8113 ) ;
#6390=AXIS2_PLACEMENT_3D ( 'NONE', #3602, #8074, #8789 ) ;
#6397=ORIENTED_EDGE ( 'NONE', *, *, #6458, .F. ) ;
#6399=ORIENTED_EDGE ( 'NONE', *, *, #6950, .F. ) ;
#6411=ORIENTED_EDGE ( 'NONE', *, *, #598, .T. ) ;
#6414=CIRCLE ( 'NONE', #6880, 8.000000000000017764 ) ;
#6426=FACE_OUTER_BOUND ( 'NONE', #6463, .T. ) ;
#6431=DIRECTION ( 'NONE',  ( 0.000000000000000000, 0.000000000000000000, 1.000000000000000000 ) ) ;
#6434=B_SPLINE_CURVE_WITH_KNOTS ( 'NONE', 3,
 ( #7694, #9173, #8982, #1780, #5351, #6167, #7645, #1013, #2608, #6837, #5534, #6976, #300, #3948 ),
 .UNSPECIFIED., .F., .F.,
 ( 4, 2, 2, 2, 2, 2, 4 ),
 ( 0.008014353914675855992, 0.01001537843003033959, 0.01101589068770758226, 0.01201640294538482492, 0.01301691520306206759, 0.01401742746073931199, 0.01601845197609379906 ),
 .UNSPECIFIED. ) ;
#6450=ORIENTED_EDGE ( 'NONE', *, *, #194, .F. ) ;
#6457=CYLINDRICAL_SURFACE ( 'NONE', #3552, 12.50000000000000000 ) ;
#6458=EDGE_CURVE ( 'NONE', #3040, #5577, #431, .T. ) ;
#6463=EDGE_LOOP ( 'NONE', ( #6539, #8600 ) ) ;
#6474=ORIENTED_EDGE ( 'NONE', *, *, #5213, .T. ) ;
#6475=LINE ( 'NONE', #1267, #5669 ) ;
#6477=DIRECTION ( 'NONE',  ( 1.000000000000000000, 0.000000000000000000, 0.000000000000000000 ) ) ;
#6479=DIRECTION ( 'NONE',  ( -0.000000000000000000, -0.000000000000000000, -1.000000000000000000 ) ) ;
#6480=EDGE_CURVE ( 'NONE', #5908, #8953, #6867, .T. ) ;
#6493=ORIENTED_EDGE ( 'NONE', *, *, #6168, .T. ) ;
#6497=EDGE_LOOP ( 'NONE', ( #3284, #8872, #1424, #834 ) ) ;
#6499=DIRECTION ( 'NONE',  ( 0.000000000000000000, 0.000000000000000000, -1.000000000000000000 ) ) ;
#6502=CARTESIAN_POINT ( 'NONE',  ( -28.66635145370234383, -1.351859493328359196, 1.696225934522937351 ) ) ;
#6505=ORIENTED_EDGE ( 'NONE', *, *, #145, .T. ) ;
#6507=CIRCLE ( 'NONE', #3277, 12.50000000000000000 ) ;
#6512=CARTESIAN_POINT ( 'NONE',  ( 22.50000000000000355, 0.000000000000000000, 10.00000000000000000 ) ) ;
#6517=AXIS2_PLACEMENT_3D ( 'NONE', #1519, #1304, #4454 ) ;
#6520=AXIS2_PLACEMENT_3D ( 'NONE', #7738, #432, #1196 ) ;
#6529=DIRECTION ( 'NONE',  ( 1.000000000000000000, 0.000000000000000000, 0.000000000000000000 ) ) ;
#6536=DIRECTION ( 'NONE',  ( 0.000000000000000000, 0.000000000000000000, -1.000000000000000000 ) ) ;
#6539=ORIENTED_EDGE ( 'NONE', *, *, #2328, .T. ) ;
#6540=ORIENTED_EDGE ( 'NONE', *, *, #2944, .F. ) ;
#6541=CARTESIAN_POINT ( 'NONE',  ( -13.50000000000000178, 1.653273178848927064E-15, 27.50000000000000355 ) ) ;
#6548=CARTESIAN_POINT ( 'NONE',  ( 16.50000000000000000, 0.000000000000000000, 2.000000000000035083 ) ) ;
#6556=CYLINDRICAL_SURFACE ( 'NONE', #1410, 15.00000000000000000 ) ;
#6557=CARTESIAN_POINT ( 'NONE',  ( 0.000000000000000000, -22.50000000000000355, 10.00000000000000000 ) ) ;
#6578=ORIENTED_EDGE ( 'NONE', *, *, #713, .T. ) ;
#6586=DIRECTION ( 'NONE',  ( -1.000000000000000000, 0.000000000000000000, 0.000000000000000000 ) ) ;
#6608=CARTESIAN_POINT ( 'NONE',  ( 8.000000000000021316, -22.50000000000000355, 0.000000000000000000 ) ) ;
#6609=CARTESIAN_POINT ( 'NONE',  ( -22.50000000000000355, 0.000000000000000000, 0.000000000000000000 ) ) ;
#6623=ORIENTED_EDGE ( 'NONE', *, *, #5675, .F. ) ;
#6624=CARTESIAN_POINT ( 'NONE',  ( 22.50000000000000355, 0.000000000000000000, 0.000000000000000000 ) ) ;
#6626=CARTESIAN_POINT ( 'NONE',  ( -2.663458823497500294, 28.40635703822599822, 1.529086667430999524 ) ) ;
#6629=FACE_OUTER_BOUND ( 'NONE', #355, .T. ) ;
#6630=CIRCLE ( 'NONE', #7699, 8.000000000000021316 ) ;
#6634=VERTEX_POINT ( 'NONE', #1225 ) ;
#6638=FACE_OUTER_BOUND ( 'NONE', #5264, .T. ) ;
#6640=CARTESIAN_POINT ( 'NONE',  ( 22.50000000000000355, 0.000000000000000000, 5.000000000000000000 ) ) ;
#6647=DIRECTION ( 'NONE',  ( 0.000000000000000000, 0.000000000000000000, 1.000000000000000000 ) ) ;
#6649=EDGE_CURVE ( 'NONE', #5465, #3092, #4884, .T. ) ;
#6652=EDGE_CURVE ( 'NONE', #8082, #6389, #4874, .T. ) ;
#6666=CARTESIAN_POINT ( 'NONE',  ( -13.50000000000000178, 1.653273178848927064E-15, 28.50000000000000355 ) ) ;
#6675=CARTESIAN_POINT ( 'NONE',  ( 4.506465992502256768, 27.73646215562212092, 1.098439957185652682 ) ) ;
#6681=CYLINDRICAL_SURFACE ( 'NONE', #6390, 6.000000000000001776 ) ;
#6682=DIRECTION ( 'NONE',  ( 0.000000000000000000, 0.000000000000000000, -1.000000000000000000 ) ) ;
#6693=DIRECTION ( 'NONE',  ( -1.000000000000000000, 0.000000000000000000, -0.000000000000000000 ) ) ;
#6695=CARTESIAN_POINT ( 'NONE',  ( 25.50000000000000355, 3.673940397442054445E-16, 10.00000000000000000 ) ) ;
#6700=ORIENTED_EDGE ( 'NONE', *, *, #2255, .T. ) ;
#6701=ORIENTED_EDGE ( 'NONE', *, *, #1961, .F. ) ;
#6716=AXIS2_PLACEMENT_3D ( 'NONE', #9408, #2748, #4900 ) ;
#6717=CARTESIAN_POINT ( 'NONE',  ( -6.000000000000000888, -22.50000000000000355, 2.000000000000013767 ) ) ;
#6719=CARTESIAN_POINT ( 'NONE',  ( 28.40858913551337750, -2.655051044735458721, 1.530521587115750037 ) ) ;
#6727=CARTESIAN_POINT ( 'NONE',  ( -4.531045531831497719, 27.74104493317181053, 1.101386028467601141 ) ) ;
#6728=AXIS2_PLACEMENT_3D ( 'NONE', #380, #4083, #3981 ) ;
#6730=CONICAL_SURFACE ( 'NONE', #4885, 6.000000000000001776, 0.7853981633974500554 ) ;
#6733=DIRECTION ( 'NONE',  ( 0.000000000000000000, 0.000000000000000000, -1.000000000000000000 ) ) ;
#6735=EDGE_LOOP ( 'NONE', ( #7058, #6033, #209, #344 ) ) ;
#6741=DIRECTION ( 'NONE',  ( 1.000000000000000000, 0.000000000000000000, 0.000000000000000000 ) ) ;
#6743=CARTESIAN_POINT ( 'NONE',  ( 0.000000000000000000, -22.50000000000000355, 5.000000000000000000 ) ) ;
#6749=DIRECTION ( 'NONE',  ( -0.000000000000000000, -0.000000000000000000, -1.000000000000000000 ) ) ;
#6756=ORIENTED_EDGE ( 'NONE', *, *, #5219, .T. ) ;
#6760=CARTESIAN_POINT ( 'NONE',  ( 0.000000000000000000, 0.000000000000000000, 0.000000000000000000 ) ) ;
#6772=CONICAL_SURFACE ( 'NONE', #7068, 6.000000000000000888, 0.7853981633974498333 ) ;
#6773=DIRECTION ( 'NONE',  ( 0.000000000000000000, 0.000000000000000000, -1.000000000000000000 ) ) ;
#6782=FACE_OUTER_BOUND ( 'NONE', #5158, .T. ) ;
#6783=DIRECTION ( 'NONE',  ( 0.000000000000000000, 0.000000000000000000, 1.000000000000000000 ) ) ;
#6811=ORIENTED_EDGE ( 'NONE', *, *, #5219, .F. ) ;
#6816=ORIENTED_EDGE ( 'NONE', *, *, #8934, .T. ) ;
#6818=EDGE_CURVE ( 'NONE', #386, #7815, #1512, .T. ) ;
#6819=CARTESIAN_POINT ( 'NONE',  ( -2.341162148116626263, 28.48643429264087246, 1.580564902411995210 ) ) ;
#6822=CARTESIAN_POINT ( 'NONE',  ( -2.651740589948411664, -28.40946940741335069, 1.531087476194299413 ) ) ;
#6825=ORIENTED_EDGE ( 'NONE', *, *, #4319, .F. ) ;
#6827=CIRCLE ( 'NONE', #525, 1.000000000000000888 ) ;
#6836=DIRECTION ( 'NONE',  ( -0.000000000000000000, -0.000000000000000000, -1.000000000000000000 ) ) ;
#6837=CARTESIAN_POINT ( 'NONE',  ( -27.44426127775441415, 5.090287965588961683, 0.9105965356992786752 ) ) ;
#6838=ORIENTED_EDGE ( 'NONE', *, *, #419, .F. ) ;
#6839=DIRECTION ( 'NONE',  ( 0.000000000000000000, 0.000000000000000000, -1.000000000000000000 ) ) ;
#6844=CARTESIAN_POINT ( 'NONE',  ( -22.50000000000000355, 0.000000000000000000, 5.000000000000000000 ) ) ;
#6859=CARTESIAN_POINT ( 'NONE',  ( 27.73557521625266631, -4.508354841688211323, 1.097869781876721795 ) ) ;
#6867=LINE ( 'NONE', #4072, #7641 ) ;
#6870=CIRCLE ( 'NONE', #7318, 1.000000000000000888 ) ;
#6873=CARTESIAN_POINT ( 'NONE',  ( 6.186958832529963814, -26.79406326810229189, 0.4926121009229034176 ) ) ;
#6874=CIRCLE ( 'NONE', #2732, 6.000000000000001776 ) ;
#6878=EDGE_CURVE ( 'NONE', #7550, #3092, #8421, .T. ) ;
#6880=AXIS2_PLACEMENT_3D ( 'NONE', #6624, #8918, #2350 ) ;
#6881=AXIS2_PLACEMENT_3D ( 'NONE', #630, #9223, #3559 ) ;
#6895=VECTOR ( 'NONE', #4449, 1000.000000000000000 ) ;
#6901=( LENGTH_UNIT ( ) NAMED_UNIT ( * ) SI_UNIT ( .MILLI., .METRE. ) );
#6909=EDGE_LOOP ( 'NONE', ( #3076, #8974 ) ) ;
#6913=DIRECTION ( 'NONE',  ( 0.000000000000000000, 0.000000000000000000, 1.000000000000000000 ) ) ;
#6917=CARTESIAN_POINT ( 'NONE',  ( 0.000000000000000000, -22.50000000000000355, 5.000000000000000000 ) ) ;
#6918=CYLINDRICAL_SURFACE ( 'NONE', #1651, 30.00000000000000000 ) ;
#6946=CARTESIAN_POINT ( 'NONE',  ( 12.50000000000000000, 1.530808498934191127E-15, 48.00000000000036948 ) ) ;
#6950=EDGE_CURVE ( 'NONE', #662, #7685, #500, .T. ) ;
#6970=AXIS2_PLACEMENT_3D ( 'NONE', #9283, #3473, #6328 ) ;
#6973=DIRECTION ( 'NONE',  ( 0.000000000000000000, 0.000000000000000000, -1.000000000000000000 ) ) ;
#6976=CARTESIAN_POINT ( 'NONE',  ( -26.78965207131482984, 6.193975265304562328, 0.4897763315595443090 ) ) ;
#6982=CIRCLE ( 'NONE', #4827, 14.49999999999998401 ) ;
#6984=CYLINDRICAL_SURFACE ( 'NONE', #3059, 6.000000000000001776 ) ;
#6995=ORIENTED_EDGE ( 'NONE', *, *, #2186, .F. ) ;
#6996=ORIENTED_EDGE ( 'NONE', *, *, #1190, .T. ) ;
#7002=EDGE_CURVE ( 'NONE', #7815, #8953, #8938, .T. ) ;
#7022=AXIS2_PLACEMENT_3D ( 'NONE', #3805, #6749, #8943 ) ;
#7034=B_SPLINE_CURVE_WITH_KNOTS ( 'NONE', 3,
 ( #4845, #1274, #5670, #1189, #1967, #2643, #470, #1230, #4127, #4170, #513, #3441, #4211, #7140 ),
 .UNSPECIFIED., .F., .F.,
 ( 4, 2, 2, 2, 2, 2, 4 ),
 ( 0.000000000000000000, 0.002003588478668952722, 0.004007176957337905444, 0.005008971196672381589, 0.006010765436006858600, 0.007012559675341334745, 0.008014353914675810889 ),
 .UNSPECIFIED. ) ;
#7046=ORIENTED_EDGE ( 'NONE', *, *, #8934, .F. ) ;
#7058=ORIENTED_EDGE ( 'NONE', *, *, #3359, .F. ) ;
#7065=ORIENTED_EDGE ( 'NONE', *, *, #5213, .F. ) ;
#7068=AXIS2_PLACEMENT_3D ( 'NONE', #5032, #3537, #2912 ) ;
#7081=CARTESIAN_POINT ( 'NONE',  ( 0.000000000000000000, 0.000000000000000000, 27.50000000000000355 ) ) ;
#7084=LINE ( 'NONE', #4743, #2822 ) ;
#7086=VERTEX_POINT ( 'NONE', #7946 ) ;
#7087=DIRECTION ( 'NONE',  ( 1.000000000000000000, 0.000000000000000000, -0.000000000000000000 ) ) ;
#7095=CARTESIAN_POINT ( 'NONE',  ( 0.000000000000000000, -22.50000000000000355, 5.000000000000000000 ) ) ;
#7098=AXIS2_PLACEMENT_3D ( 'NONE', #9189, #7849, #1214 ) ;
#7105=ADVANCED_FACE ( 'NONE', ( #3378 ), #7717, .F. ) ;
#7110=EDGE_CURVE ( 'NONE', #1940, #5539, #8780, .T. ) ;
#7111=FACE_OUTER_BOUND ( 'NONE', #2774, .T. ) ;
#7113=CARTESIAN_POINT ( 'NONE',  ( -28.21791960234945051, -3.296518076058942093, 1.407948315796079486 ) ) ;
#7122=PLANE ( 'NONE',  #2241 ) ;
#7124=ADVANCED_FACE ( 'NONE', ( #4340, #67 ), #5254, .T. ) ;
#7130=ADVANCED_FACE ( 'NONE', ( #3616 ), #6556, .T. ) ;
#7140=CARTESIAN_POINT ( 'NONE',  ( 28.75000000000001776, 7.654042494438380704E-16, 1.750000000000019762 ) ) ;
#7147=EDGE_CURVE ( 'NONE', #6634, #3040, #8895, .T. ) ;
#7148=FACE_OUTER_BOUND ( 'NONE', #8856, .T. ) ;
#7162=CARTESIAN_POINT ( 'NONE',  ( -26.79453276911117854, -6.186305604711966666, 0.4929139230000563754 ) ) ;
#7167=ORIENTED_EDGE ( 'NONE', *, *, #8816, .F. ) ;
#7176=DIRECTION ( 'NONE',  ( 1.000000000000000000, 0.000000000000000000, 0.000000000000000000 ) ) ;
#7187=FACE_OUTER_BOUND ( 'NONE', #1814, .T. ) ;
#7210=CARTESIAN_POINT ( 'NONE',  ( -27.45147183906051680, -5.102343880922198593, 0.9152318965389161232 ) ) ;
#7214=ORIENTED_EDGE ( 'NONE', *, *, #1713, .T. ) ;
#7215=DIRECTION ( 'NONE',  ( 0.000000000000000000, 0.000000000000000000, 1.000000000000000000 ) ) ;
#7232=EDGE_CURVE ( 'NONE', #7477, #1471, #5727, .T. ) ;
#7238=VECTOR ( 'NONE', #8172, 1000.000000000000000 ) ;
#7244=CARTESIAN_POINT ( 'NONE',  ( 0.000000000000000000, 0.000000000000000000, 28.50000000000000355 ) ) ;
#7255=DIRECTION ( 'NONE',  ( -0.000000000000000000, -0.000000000000000000, -1.000000000000000000 ) ) ;
#7260=ORIENTED_EDGE ( 'NONE', *, *, #5540, .F. ) ;
#7268=DIRECTION ( 'NONE',  ( -0.000000000000000000, -0.000000000000000000, -1.000000000000000000 ) ) ;
#7285=DIRECTION ( 'NONE',  ( 0.7071067811865486830, 8.659560562354948882E-17, -0.7071067811865464625 ) ) ;
#7291=FACE_OUTER_BOUND ( 'NONE', #7529, .T. ) ;
#7302=PRODUCT_DEFINITION_SHAPE ( 'NONE', 'NONE',  #2939 ) ;
#7312=DIRECTION ( 'NONE',  ( -1.000000000000000000, 0.000000000000000000, 0.000000000000000000 ) ) ;
#7314=AXIS2_PLACEMENT_3D ( 'NONE', #686, #6536, #25 ) ;
#7316=AXIS2_PLACEMENT_3D ( 'NONE', #6019, #8940, #2744 ) ;
#7318=AXIS2_PLACEMENT_3D ( 'NONE', #1690, #2556, #6121 ) ;
#7319=ORIENTED_EDGE ( 'NONE', *, *, #6266, .T. ) ;
#7320=CARTESIAN_POINT ( 'NONE',  ( 0.000000000000000000, 0.000000000000000000, 50.00000000000000000 ) ) ;
#7322=VERTEX_POINT ( 'NONE', #8945 ) ;
#7325=CARTESIAN_POINT ( 'NONE',  ( 26.02777777777776791, 7.180166011355005651, 0.000000000000000000 ) ) ;
#7333=ORIENTED_EDGE ( 'NONE', *, *, #2959, .T. ) ;
#7352=DIRECTION ( 'NONE',  ( -1.000000000000000000, 0.000000000000000000, 0.000000000000000000 ) ) ;
#7354=CARTESIAN_POINT ( 'NONE',  ( 0.000000000000000000, 22.50000000000000355, 5.000000000000000000 ) ) ;
#7358=EDGE_CURVE ( 'NONE', #4158, #7976, #4677, .T. ) ;
#7361=DIRECTION ( 'NONE',  ( 1.000000000000000000, 0.000000000000000000, 0.000000000000000000 ) ) ;
#7379=ORIENTED_EDGE ( 'NONE', *, *, #488, .T. ) ;
#7391=ORIENTED_EDGE ( 'NONE', *, *, #3530, .F. ) ;
#7395=CARTESIAN_POINT ( 'NONE',  ( 0.000000000000000000, 22.50000000000000355, 2.000000000000013767 ) ) ;
#7397=CIRCLE ( 'NONE', #3406, 2.999999999999999112 ) ;
#7399=EDGE_CURVE ( 'NONE', #1766, #450, #7397, .T. ) ;
#7408=AXIS2_PLACEMENT_3D ( 'NONE', #501, #7501, #9431 ) ;
#7426=CIRCLE ( 'NONE', #5282, 26.99999999999999645 ) ;
#7431=B_SPLINE_CURVE_WITH_KNOTS ( 'NONE', 3,
 ( #2758, #2029, #7162, #7210, #1395, #9373, #7113, #9322, #2706, #4333, #6502, #2799, #9420, #7932 ),
 .UNSPECIFIED., .F., .F.,
 ( 4, 2, 2, 2, 2, 2, 4 ),
 ( 0.000000000000000000, 0.002003588478668964865, 0.004007176957337929731, 0.005008971196672411079, 0.006010765436006893295, 0.007012559675341373776, 0.008014353914675855992 ),
 .UNSPECIFIED. ) ;
#7437=EDGE_LOOP ( 'NONE', ( #1276, #8329, #7720, #7969 ) ) ;
#7440=CARTESIAN_POINT ( 'NONE',  ( 28.50000000000000355, 7.347880794884123680E-16, 2.000000000000035083 ) ) ;
#7445=DIRECTION ( 'NONE',  ( -1.000000000000000000, 0.000000000000000000, 0.000000000000000000 ) ) ;
#7448=LINE ( 'NONE', #1643, #1271 ) ;
#7456=AXIS2_PLACEMENT_3D ( 'NONE', #1896, #4641, #4822 ) ;
#7464=ADVANCED_FACE ( 'NONE', ( #1980 ), #7838, .T. ) ;
#7469=CARTESIAN_POINT ( 'NONE',  ( -16.50000000000000000, 7.347880794884123680E-16, 2.000000000000039080 ) ) ;
#7477=VERTEX_POINT ( 'NONE', #1155 ) ;
#7481=VERTEX_POINT ( 'NONE', #1246 ) ;
#7482=CARTESIAN_POINT ( 'NONE',  ( 5.373124232108025033, 27.28744256482707087, 0.8097845059602708506 ) ) ;
#7484=VECTOR ( 'NONE', #2048, 1000.000000000000000 ) ;
#7487=CARTESIAN_POINT ( 'NONE',  ( 1.356121383298963590, -28.66577847273270763, 1.695857589613878558 ) ) ;
#7501=DIRECTION ( 'NONE',  ( -0.000000000000000000, -0.000000000000000000, -1.000000000000000000 ) ) ;
#7503=ORIENTED_EDGE ( 'NONE', *, *, #8571, .T. ) ;
#7527=CARTESIAN_POINT ( 'NONE',  ( 19.50000000000000355, 0.000000000000000000, 10.00000000000000000 ) ) ;
#7529=EDGE_LOOP ( 'NONE', ( #576, #8788, #3344, #5656, #4758 ) ) ;
#7539=CARTESIAN_POINT ( 'NONE',  ( -0.6691251631324991456, -28.75033890800110825, 1.750217869429287365 ) ) ;
#7550=VERTEX_POINT ( 'NONE', #722 ) ;
#7563=DIRECTION ( 'NONE',  ( 1.000000000000000000, 0.000000000000000000, 0.000000000000000000 ) ) ;
#7569=CARTESIAN_POINT ( 'NONE',  ( -30.00000000000000000, 0.000000000000000000, 10.00000000000000000 ) ) ;
#7570=CYLINDRICAL_SURFACE ( 'NONE', #6970, 3.000000000000000000 ) ;
#7581=AXIS2_PLACEMENT_3D ( 'NONE', #2545, #8348, #4704 ) ;
#7603=VERTEX_POINT ( 'NONE', #6541 ) ;
#7607=( NAMED_UNIT ( * ) PLANE_ANGLE_UNIT ( ) SI_UNIT ( $, .RADIAN. ) );
#7611=DIRECTION ( 'NONE',  ( 0.000000000000000000, 0.000000000000000000, -1.000000000000000000 ) ) ;
#7614=DIRECTION ( 'NONE',  ( -1.000000000000000000, 0.000000000000000000, 0.000000000000000000 ) ) ;
#7620=ORIENTED_EDGE ( 'NONE', *, *, #9320, .T. ) ;
#7630=DIRECTION ( 'NONE',  ( -1.000000000000000000, 0.000000000000000000, 0.000000000000000000 ) ) ;
#7631=CARTESIAN_POINT ( 'NONE',  ( 3.299340129088522922, -28.21697752735853726, 1.407342696159064488 ) ) ;
#7638=EDGE_CURVE ( 'NONE', #5792, #9435, #5472, .T. ) ;
#7641=VECTOR ( 'NONE', #4028, 1000.000000000000000 ) ;
#7645=CARTESIAN_POINT ( 'NONE',  ( -28.11123945536280644, 3.602653646940651377, 1.339368221304670037 ) ) ;
#7648=ADVANCED_FACE ( 'NONE', ( #2208 ), #6681, .F. ) ;
#7651=VERTEX_POINT ( 'NONE', #3698 ) ;
#7672=CARTESIAN_POINT ( 'NONE',  ( 28.75000000000001776, 7.654042494438380704E-16, 1.750000000000019762 ) ) ;
#7676=DIRECTION ( 'NONE',  ( -1.000000000000000000, 0.000000000000000000, 0.000000000000000000 ) ) ;
#7679=DIRECTION ( 'NONE',  ( 1.000000000000000000, 0.000000000000000000, 0.000000000000000000 ) ) ;
#7685=VERTEX_POINT ( 'NONE', #6296 ) ;
#7694=CARTESIAN_POINT ( 'NONE',  ( -28.75000000000002132, 2.329604860730800488E-26, 1.750000000000023537 ) ) ;
#7699=AXIS2_PLACEMENT_3D ( 'NONE', #1159, #8429, #3373 ) ;
#7707=CIRCLE ( 'NONE', #5092, 3.000000000000000000 ) ;
#7711=ORIENTED_EDGE ( 'NONE', *, *, #5990, .T. ) ;
#7717=TOROIDAL_SURFACE ( 'NONE', #3568, 13.50000000000000178, 1.000000000000000000 ) ;
#7718=DIRECTION ( 'NONE',  ( -0.000000000000000000, -0.000000000000000000, -1.000000000000000000 ) ) ;
#7720=ORIENTED_EDGE ( 'NONE', *, *, #2186, .T. ) ;
#7722=ORIENTED_EDGE ( 'NONE', *, *, #3139, .F. ) ;
#7726=ORIENTED_EDGE ( 'NONE', *, *, #774, .F. ) ;
#7731=CARTESIAN_POINT ( 'NONE',  ( -22.50000000000000355, 0.000000000000000000, 5.000000000000000000 ) ) ;
#7738=CARTESIAN_POINT ( 'NONE',  ( -22.50000000000000355, 0.000000000000000000, 10.00000000000000000 ) ) ;
#7748=ADVANCED_FACE ( 'NONE', ( #6782 ), #4614, .F. ) ;
#7751=CARTESIAN_POINT ( 'NONE',  ( -8.000000000000021316, -22.50000000000000355, 0.000000000000000000 ) ) ;
#7765=EDGE_LOOP ( 'NONE', ( #8752, #7379, #2657, #9432, #6292, #7711, #376, #8018, #1447, #6756, #4214, #1353, #3161, #5984 ) ) ;
#7781=AXIS2_PLACEMENT_3D ( 'NONE', #8087, #3670, #7361 ) ;
#7786=AXIS2_PLACEMENT_3D ( 'NONE', #9453, #6733, #2970 ) ;
#7795=DIRECTION ( 'NONE',  ( 0.000000000000000000, 0.000000000000000000, 1.000000000000000000 ) ) ;
#7800=ORIENTED_EDGE ( 'NONE', *, *, #1576, .T. ) ;
#7813=CARTESIAN_POINT ( 'NONE',  ( 0.000000000000000000, 0.000000000000000000, 27.50000000000000355 ) ) ;
#7815=VERTEX_POINT ( 'NONE', #7440 ) ;
#7816=LINE ( 'NONE', #8001, #6895 ) ;
#7818=CARTESIAN_POINT ( 'NONE',  ( 0.000000000000000000, 0.000000000000000000, 10.00000000000000000 ) ) ;
#7838=PLANE ( 'NONE',  #6028 ) ;
#7840=CARTESIAN_POINT ( 'NONE',  ( -11.96410161513786008, 0.000000000000000000, 50.00000000000000000 ) ) ;
#7849=DIRECTION ( 'NONE',  ( 0.000000000000000000, 0.000000000000000000, -1.000000000000000000 ) ) ;
#7852=DIRECTION ( 'NONE',  ( 0.000000000000000000, 0.000000000000000000, -1.000000000000000000 ) ) ;
#7860=CARTESIAN_POINT ( 'NONE',  ( 30.00000000000000000, 3.673940397442059178E-15, 10.00000000000000000 ) ) ;
#7862=CARTESIAN_POINT ( 'NONE',  ( 0.000000000000000000, 0.000000000000000000, 10.00000000000000000 ) ) ;
#7874=CARTESIAN_POINT ( 'NONE',  ( -22.50000000000000355, 0.000000000000000000, 10.00000000000000000 ) ) ;
#7882=EDGE_CURVE ( 'NONE', #1471, #7477, #4388, .T. ) ;
#7887=CIRCLE ( 'NONE', #3746, 6.000000000000001776 ) ;
#7898=DIRECTION ( 'NONE',  ( 1.000000000000000000, 0.000000000000000000, 0.000000000000000000 ) ) ;
#7903=DIRECTION ( 'NONE',  ( 0.7071067811865487940, 8.659560562354950115E-17, -0.7071067811865463515 ) ) ;
#7913=ORIENTED_EDGE ( 'NONE', *, *, #613, .T. ) ;
#7931=LINE ( 'NONE', #1932, #5193 ) ;
#7932=CARTESIAN_POINT ( 'NONE',  ( -28.75000000000002132, 2.329604860730800488E-26, 1.750000000000023537 ) ) ;
#7933=EDGE_CURVE ( 'NONE', #672, #3936, #5922, .T. ) ;
#7944=ORIENTED_EDGE ( 'NONE', *, *, #3711, .T. ) ;
#7946=CARTESIAN_POINT ( 'NONE',  ( 19.50000000000000355, 0.000000000000000000, 10.00000000000000000 ) ) ;
#7949=CARTESIAN_POINT ( 'NONE',  ( -6.000000000000000888, 22.50000000000000355, 2.000000000000013767 ) ) ;
#7959=DIRECTION ( 'NONE',  ( -1.000000000000000000, 0.000000000000000000, 0.000000000000000000 ) ) ;
#7965=AXIS2_PLACEMENT_3D ( 'NONE', #5094, #7255, #5245 ) ;
#7968=DIRECTION ( 'NONE',  ( -1.000000000000000000, 0.000000000000000000, 0.000000000000000000 ) ) ;
#7969=ORIENTED_EDGE ( 'NONE', *, *, #1413, .F. ) ;
#7973=CARTESIAN_POINT ( 'NONE',  ( 11.96410161513786008, 1.497994186849708771E-15, 50.00000000000000000 ) ) ;
#7974=CARTESIAN_POINT ( 'NONE',  ( 0.000000000000000000, -22.50000000000000355, 2.000000000000013767 ) ) ;
#7976=VERTEX_POINT ( 'NONE', #4451 ) ;
#7989=DIRECTION ( 'NONE',  ( -1.000000000000000000, 0.000000000000000000, 0.000000000000000000 ) ) ;
#7998=VERTEX_POINT ( 'NONE', #4492 ) ;
#8001=CARTESIAN_POINT ( 'NONE',  ( 30.00000000000000000, 0.000000000000000000, 2.999999999999999112 ) ) ;
#8004=CIRCLE ( 'NONE', #5404, 8.000000000000047962 ) ;
#8018=ORIENTED_EDGE ( 'NONE', *, *, #5890, .T. ) ;
#8025=CARTESIAN_POINT ( 'NONE',  ( 22.50000000000000355, 0.000000000000000000, 5.000000000000000000 ) ) ;
#8026=AXIS2_PLACEMENT_3D ( 'NONE', #6512, #7268, #2904 ) ;
#8034=DIRECTION ( 'NONE',  ( -0.000000000000000000, -0.000000000000000000, -1.000000000000000000 ) ) ;
#8050=FACE_OUTER_BOUND ( 'NONE', #2202, .T. ) ;
#8057=ADVANCED_FACE ( 'NONE', ( #8812 ), #129, .F. ) ;
#8058=EDGE_LOOP ( 'NONE', ( #987, #1356, #743, #735 ) ) ;
#8059=CARTESIAN_POINT ( 'NONE',  ( 6.000000000000000888, -22.50000000000000355, 2.000000000000013767 ) ) ;
#8060=ADVANCED_BREP_SHAPE_REPRESENTATION ( '', ( #4990, #1614 ), #1322 ) ;
#8064=DIRECTION ( 'NONE',  ( 0.000000000000000000, 0.000000000000000000, -1.000000000000000000 ) ) ;
#8074=DIRECTION ( 'NONE',  ( -0.000000000000000000, -0.000000000000000000, -1.000000000000000000 ) ) ;
#8079=DIRECTION ( 'NONE',  ( 0.000000000000000000, 0.000000000000000000, -1.000000000000000000 ) ) ;
#8080=DIRECTION ( 'NONE',  ( 0.000000000000000000, 0.000000000000000000, -1.000000000000000000 ) ) ;
#8082=VERTEX_POINT ( 'NONE', #8958 ) ;
#8083=AXIS2_PLACEMENT_3D ( 'NONE', #8908, #3058, #5270 ) ;
#8084=DIRECTION ( 'NONE',  ( -0.000000000000000000, -0.000000000000000000, -1.000000000000000000 ) ) ;
#8087=CARTESIAN_POINT ( 'NONE',  ( 22.50000000000000355, 0.000000000000000000, 2.000000000000035083 ) ) ;
#8105=DIRECTION ( 'NONE',  ( 1.000000000000000000, 0.000000000000000000, 0.000000000000000000 ) ) ;
#8113=CARTESIAN_POINT ( 'NONE',  ( -6.000000000000000888, 22.50000000000000355, 2.000000000000013767 ) ) ;
#8115=CARTESIAN_POINT ( 'NONE',  ( -6.697288230627575167, 26.42764960499151528, 0.2570604603516986608 ) ) ;
#8124=ORIENTED_EDGE ( 'NONE', *, *, #4830, .T. ) ;
#8125=EDGE_LOOP ( 'NONE', ( #1087, #5584, #6450, #5136 ) ) ;
#8136=DIRECTION ( 'NONE',  ( 1.000000000000000000, 0.000000000000000000, 0.000000000000000000 ) ) ;
#8145=ORIENTED_EDGE ( 'NONE', *, *, #7110, .T. ) ;
#8163=CARTESIAN_POINT ( 'NONE',  ( 4.208878922505766340, 27.87018698802495464, 1.184405920873192075 ) ) ;
#8170=DIRECTION ( 'NONE',  ( 1.000000000000000000, 0.000000000000000000, 0.000000000000000000 ) ) ;
#8172=DIRECTION ( 'NONE',  ( -0.7071067811865512365, 0.000000000000000000, -0.7071067811865439090 ) ) ;
#8174=DIRECTION ( 'NONE',  ( -1.000000000000000000, 0.000000000000000000, 0.000000000000000000 ) ) ;
#8204=AXIS2_PLACEMENT_3D ( 'NONE', #7874, #1281, #4219 ) ;
#8208=CARTESIAN_POINT ( 'NONE',  ( 2.663458823497500294, -28.40635703822599822, 1.529086667430999524 ) ) ;
#8209=ORIENTED_EDGE ( 'NONE', *, *, #613, .F. ) ;
#8215=DIRECTION ( 'NONE',  ( -0.000000000000000000, -0.000000000000000000, -1.000000000000000000 ) ) ;
#8218=ADVANCED_FACE ( 'NONE', ( #2440 ), #6098, .F. ) ;
#8222=EDGE_LOOP ( 'NONE', ( #8388, #7214 ) ) ;
#8231=EDGE_CURVE ( 'NONE', #672, #5549, #401, .T. ) ;
#8235=ADVANCED_FACE ( 'NONE', ( #1707 ), #1168, .T. ) ;
#8249=VECTOR ( 'NONE', #7285, 1000.000000000000000 ) ;
#8259=CARTESIAN_POINT ( 'NONE',  ( 6.000000000000000888, 22.50000000000000355, 5.000000000000000000 ) ) ;
#8261=CARTESIAN_POINT ( 'NONE',  ( 0.6691251631324991456, 28.75033890800110825, 1.750217869429287365 ) ) ;
#8289=ADVANCED_FACE ( 'NONE', ( #9278 ), #7122, .F. ) ;
#8294=ORIENTED_EDGE ( 'NONE', *, *, #2433, .T. ) ;
#8300=LINE ( 'NONE', #4651, #2625 ) ;
#8316=CARTESIAN_POINT ( 'NONE',  ( -19.50000000000000355, 3.673940397442054445E-16, 10.00000000000000000 ) ) ;
#8319=CARTESIAN_POINT ( 'NONE',  ( -15.00000000000000000, 0.000000000000000000, 27.50000000000000355 ) ) ;
#8329=ORIENTED_EDGE ( 'NONE', *, *, #2315, .T. ) ;
#8332=CARTESIAN_POINT ( 'NONE',  ( -22.50000000000000355, 0.000000000000000000, 2.000000000000039080 ) ) ;
#8348=DIRECTION ( 'NONE',  ( -0.000000000000000000, -0.000000000000000000, -1.000000000000000000 ) ) ;
#8349=DIRECTION ( 'NONE',  ( -1.000000000000000000, 0.000000000000000000, 0.000000000000000000 ) ) ;
#8350=ORIENTED_EDGE ( 'NONE', *, *, #2959, .F. ) ;
#8359=APPLICATION_CONTEXT ( 'automotive_design' ) ;
#8362=DIRECTION ( 'NONE',  ( 0.7071067811865486830, 8.659560562354948882E-17, -0.7071067811865464625 ) ) ;
#8363=EDGE_CURVE ( 'NONE', #9459, #2492, #1955, .T. ) ;
#8364=DIRECTION ( 'NONE',  ( -1.000000000000000000, 0.000000000000000000, 0.000000000000000000 ) ) ;
#8387=CARTESIAN_POINT ( 'NONE',  ( 28.48969330601476813, -2.327370969396562295, 1.582659982438076263 ) ) ;
#8388=ORIENTED_EDGE ( 'NONE', *, *, #9460, .T. ) ;
#8399=CONICAL_SURFACE ( 'NONE', #4251, 6.000000000000001776, 0.7853981633974431720 ) ;
#8402=DIRECTION ( 'NONE',  ( -0.000000000000000000, -0.000000000000000000, -1.000000000000000000 ) ) ;
#8413=EDGE_CURVE ( 'NONE', #8953, #7815, #871, .T. ) ;
#8414=EDGE_CURVE ( 'NONE', #4536, #7086, #1034, .T. ) ;
#8421=CIRCLE ( 'NONE', #5877, 15.00000000000000000 ) ;
#8425=DIRECTION ( 'NONE',  ( 0.000000000000000000, 0.000000000000000000, -1.000000000000000000 ) ) ;
#8429=DIRECTION ( 'NONE',  ( 0.000000000000000000, 0.000000000000000000, 1.000000000000000000 ) ) ;
#8451=ADVANCED_FACE ( 'NONE', ( #3617 ), #68, .F. ) ;
#8454=CYLINDRICAL_SURFACE ( 'NONE', #8711, 6.000000000000000888 ) ;
#8455=ORIENTED_EDGE ( 'NONE', *, *, #3222, .T. ) ;
#8465=LINE ( 'NONE', #5537, #277 ) ;
#8512=PLANE ( 'NONE',  #117 ) ;
#8521=VECTOR ( 'NONE', #8966, 1000.000000000000000 ) ;
#8531=FACE_OUTER_BOUND ( 'NONE', #3638, .T. ) ;
#8541=EDGE_CURVE ( 'NONE', #7550, #7477, #2376, .T. ) ;
#8549=DIRECTION ( 'NONE',  ( 1.000000000000000000, 1.776356839400250465E-15, 0.000000000000000000 ) ) ;
#8560=DIRECTION ( 'NONE',  ( -1.000000000000000000, 0.000000000000000000, -0.000000000000000000 ) ) ;
#8565=VECTOR ( 'NONE', #4450, 1000.000000000000000 ) ;
#8571=EDGE_CURVE ( 'NONE', #3040, #3178, #259, .T. ) ;
#8581=ORIENTED_EDGE ( 'NONE', *, *, #6878, .F. ) ;
#8582=CARTESIAN_POINT ( 'NONE',  ( -28.75000000000002132, 2.329604860730800488E-26, 1.750000000000023537 ) ) ;
#8586=LINE ( 'NONE', #2005, #373 ) ;
#8597=ORIENTED_EDGE ( 'NONE', *, *, #462, .F. ) ;
#8600=ORIENTED_EDGE ( 'NONE', *, *, #5675, .T. ) ;
#8603=LINE ( 'NONE', #7840, #5044 ) ;
#8605=CARTESIAN_POINT ( 'NONE',  ( 0.000000000000000000, 0.000000000000000000, 50.00000000000000000 ) ) ;
#8611=AXIS2_PLACEMENT_3D ( 'NONE', #3091, #739, #6030 ) ;
#8630=DIRECTION ( 'NONE',  ( -0.000000000000000000, -0.000000000000000000, -1.000000000000000000 ) ) ;
#8631=CARTESIAN_POINT ( 'NONE',  ( -5.373124232108025033, -27.28744256482707087, 0.8097845059602708506 ) ) ;
#8647=ORIENTED_EDGE ( 'NONE', *, *, #5844, .F. ) ;
#8680=CARTESIAN_POINT ( 'NONE',  ( 0.000000000000000000, 22.50000000000000355, 5.000000000000000000 ) ) ;
#8682=EDGE_LOOP ( 'NONE', ( #346, #6378, #6474, #9412 ) ) ;
#8686=AXIS2_PLACEMENT_3D ( 'NONE', #8332, #7611, #1751 ) ;
#8697=ADVANCED_FACE ( 'NONE', ( #9370, #7111 ), #8512, .T. ) ;
#8702=CIRCLE ( 'NONE', #4719, 30.00000000000000000 ) ;
#8705=CIRCLE ( 'NONE', #6113, 6.000000000000001776 ) ;
#8711=AXIS2_PLACEMENT_3D ( 'NONE', #7095, #1867, #6300 ) ;
#8714=CIRCLE ( 'NONE', #6728, 8.000000000000021316 ) ;
#8722=ORIENTED_EDGE ( 'NONE', *, *, #8363, .F. ) ;
#8743=ORIENTED_EDGE ( 'NONE', *, *, #7933, .T. ) ;
#8744=ORIENTED_EDGE ( 'NONE', *, *, #308, .F. ) ;
#8747=CARTESIAN_POINT ( 'NONE',  ( -12.50000000000000000, 0.000000000000000000, 28.50000000000000355 ) ) ;
#8748=LINE ( 'NONE', #3850, #7238 ) ;
#8749=PLANE ( 'NONE',  #1680 ) ;
#8752=ORIENTED_EDGE ( 'NONE', *, *, #4026, .T. ) ;
#8766=DIRECTION ( 'NONE',  ( 1.000000000000000000, 0.000000000000000000, 0.000000000000000000 ) ) ;
#8772=CARTESIAN_POINT ( 'NONE',  ( -3.000000000000000000, -22.50000000000000355, 5.000000000000000000 ) ) ;
#8780=CIRCLE ( 'NONE', #3562, 3.000000000000000000 ) ;
#8788=ORIENTED_EDGE ( 'NONE', *, *, #8413, .F. ) ;
#8789=DIRECTION ( 'NONE',  ( -1.000000000000000000, 0.000000000000000000, 0.000000000000000000 ) ) ;
#8798=CARTESIAN_POINT ( 'NONE',  ( 0.000000000000000000, 0.000000000000000000, 27.50000000000000355 ) ) ;
#8809=EDGE_CURVE ( 'NONE', #7685, #2348, #4108, .T. ) ;
#8812=FACE_OUTER_BOUND ( 'NONE', #5490, .T. ) ;
#8816=EDGE_CURVE ( 'NONE', #386, #5908, #8705, .T. ) ;
#8826=CARTESIAN_POINT ( 'NONE',  ( 6.193323906411744240, 26.79012200670185351, 0.4900784328797758715 ) ) ;
#8832=ORIENTED_EDGE ( 'NONE', *, *, #7232, .F. ) ;
#8833=EDGE_CURVE ( 'NONE', #7481, #152, #2735, .T. ) ;
#8841=DIRECTION ( 'NONE',  ( -1.000000000000000000, 0.000000000000000000, 0.000000000000000000 ) ) ;
#8845=VERTEX_POINT ( 'NONE', #2163 ) ;
#8847=DIRECTION ( 'NONE',  ( -0.000000000000000000, -0.000000000000000000, -1.000000000000000000 ) ) ;
#8856=EDGE_LOOP ( 'NONE', ( #6085, #3912, #4326, #7046 ) ) ;
#8870=DIRECTION ( 'NONE',  ( 0.000000000000000000, 0.000000000000000000, -1.000000000000000000 ) ) ;
#8872=ORIENTED_EDGE ( 'NONE', *, *, #2766, .F. ) ;
#8879=ADVANCED_FACE ( 'NONE', ( #6638 ), #9158, .F. ) ;
#8889=DIRECTION ( 'NONE',  ( 0.000000000000000000, 0.000000000000000000, -1.000000000000000000 ) ) ;
#8893=ORIENTED_EDGE ( 'NONE', *, *, #2143, .T. ) ;
#8895=LINE ( 'NONE', #2854, #4795 ) ;
#8899=AXIS2_PLACEMENT_3D ( 'NONE', #4753, #288, #1088 ) ;
#8908=CARTESIAN_POINT ( 'NONE',  ( 0.000000000000000000, -22.50000000000000355, 10.00000000000000000 ) ) ;
#8918=DIRECTION ( 'NONE',  ( 0.000000000000000000, 0.000000000000000000, 1.000000000000000000 ) ) ;
#8924=DIRECTION ( 'NONE',  ( -0.000000000000000000, -0.000000000000000000, -1.000000000000000000 ) ) ;
#8931=DIRECTION ( 'NONE',  ( -0.000000000000000000, -0.000000000000000000, -1.000000000000000000 ) ) ;
#8934=EDGE_CURVE ( 'NONE', #9435, #6389, #11, .T. ) ;
#8937=CARTESIAN_POINT ( 'NONE',  ( -28.50000000000000355, 0.000000000000000000, 2.000000000000039080 ) ) ;
#8938=CIRCLE ( 'NONE', #7098, 6.000000000000001776 ) ;
#8940=DIRECTION ( 'NONE',  ( -0.000000000000000000, -0.000000000000000000, -1.000000000000000000 ) ) ;
#8943=DIRECTION ( 'NONE',  ( 1.000000000000000000, 0.000000000000000000, 0.000000000000000000 ) ) ;
#8945=CARTESIAN_POINT ( 'NONE',  ( -12.50000000000000000, 0.000000000000000000, 48.00000000000036948 ) ) ;
#8946=DIRECTION ( 'NONE',  ( 0.000000000000000000, 0.000000000000000000, -1.000000000000000000 ) ) ;
#8948=AXIS2_PLACEMENT_3D ( 'NONE', #1172, #6233, #3342 ) ;
#8949=EDGE_CURVE ( 'NONE', #9261, #5549, #5943, .T. ) ;
#8953=VERTEX_POINT ( 'NONE', #860 ) ;
#8958=CARTESIAN_POINT ( 'NONE',  ( 6.000000000000000888, 22.50000000000000355, 2.000000000000013767 ) ) ;
#8959=CONICAL_SURFACE ( 'NONE', #3134, 30.00000000000000000, 0.7853981633974488341 ) ;
#8962=CARTESIAN_POINT ( 'NONE',  ( 26.02777777777776436, -7.180166011355007427, 0.000000000000000000 ) ) ;
#8965=ORIENTED_EDGE ( 'NONE', *, *, #2328, .F. ) ;
#8966=DIRECTION ( 'NONE',  ( -0.000000000000000000, -0.000000000000000000, -1.000000000000000000 ) ) ;
#8968=FACE_BOUND ( 'NONE', #5, .T. ) ;
#8974=ORIENTED_EDGE ( 'NONE', *, *, #6218, .F. ) ;
#8975=ORIENTED_EDGE ( 'NONE', *, *, #3931, .T. ) ;
#8982=CARTESIAN_POINT ( 'NONE',  ( -28.68405123480335916, 1.339801352072197860, 1.707604365230749766 ) ) ;
#8984=EDGE_CURVE ( 'NONE', #933, #3742, #9314, .T. ) ;
#8988=AXIS2_PLACEMENT_3D ( 'NONE', #7862, #4166, #2090 ) ;
#8992=CARTESIAN_POINT ( 'NONE',  ( 6.000000000000000888, 22.50000000000000355, 5.000000000000000000 ) ) ;
#8995=MECHANICAL_DESIGN_GEOMETRIC_PRESENTATION_REPRESENTATION('',(#6078),#2391);
#9011=CARTESIAN_POINT ( 'NONE',  ( 27.28672223502584160, -5.374373886926188781, 0.8093214368023355920 ) ) ;
#9012=AXIS2_PLACEMENT_3D ( 'NONE', #5192, #2977, #2118 ) ;
#9018=DIRECTION ( 'NONE',  ( -0.000000000000000000, -0.000000000000000000, -1.000000000000000000 ) ) ;
#9020=CARTESIAN_POINT ( 'NONE',  ( 19.50000000000000355, 0.000000000000000000, 5.000000000000000000 ) ) ;
#9023=CARTESIAN_POINT ( 'NONE',  ( 7.180166011355011868, -26.02777777777776436, 0.000000000000000000 ) ) ;
#9050=ADVANCED_FACE ( 'NONE', ( #4666 ), #1688, .F. ) ;
#9058=CARTESIAN_POINT ( 'NONE',  ( 27.86926932341927809, -4.210987672173456708, 1.183815993626684104 ) ) ;
#9064=DIRECTION ( 'NONE',  ( -0.000000000000000000, -0.000000000000000000, -1.000000000000000000 ) ) ;
#9074=CARTESIAN_POINT ( 'NONE',  ( -22.50000000000000355, 0.000000000000000000, 5.000000000000000000 ) ) ;
#9083=CARTESIAN_POINT ( 'NONE',  ( -6.000000000000000888, -22.50000000000000355, 2.000000000000013767 ) ) ;
#9084=AXIS2_PLACEMENT_3D ( 'NONE', #1451, #6647, #2274 ) ;
#9091=ORIENTED_EDGE ( 'NONE', *, *, #9436, .F. ) ;
#9116=VERTEX_POINT ( 'NONE', #1919 ) ;
#9117=PRODUCT_CONTEXT ( 'NONE', #2785, 'mechanical' ) ;
#9133=ORIENTED_EDGE ( 'NONE', *, *, #4823, .F. ) ;
#9134=ORIENTED_EDGE ( 'NONE', *, *, #7882, .T. ) ;
#9137=CARTESIAN_POINT ( 'NONE',  ( 0.000000000000000000, 0.000000000000000000, 26.99999999999999289 ) ) ;
#9147=ORIENTED_EDGE ( 'NONE', *, *, #1831, .F. ) ;
#9148=CARTESIAN_POINT ( 'NONE',  ( -30.00000000000000000, 0.000000000000000000, 2.999999999999999112 ) ) ;
#9151=DIRECTION ( 'NONE',  ( 1.000000000000000000, 0.000000000000000000, -0.000000000000000000 ) ) ;
#9158=CONICAL_SURFACE ( 'NONE', #3962, 6.000000000000000888, 0.7853981633974498333 ) ;
#9160=CARTESIAN_POINT ( 'NONE',  ( -5.088821267330767562, -27.44505377838575200, 0.9111060003908462157 ) ) ;
#9172=CARTESIAN_POINT ( 'NONE',  ( 3.000000000000000000, -22.50000000000000355, 10.00000000000000000 ) ) ;
#9173=CARTESIAN_POINT ( 'NONE',  ( -28.75000000000002842, 0.6738334415499688257, 1.750000000000029754 ) ) ;
#9174=EDGE_LOOP ( 'NONE', ( #7333, #976 ) ) ;
#9182=CARTESIAN_POINT ( 'NONE',  ( 22.50000000000000355, 0.000000000000000000, 5.000000000000000000 ) ) ;
#9189=CARTESIAN_POINT ( 'NONE',  ( 22.50000000000000355, 0.000000000000000000, 2.000000000000035083 ) ) ;
#9203=AXIS2_PLACEMENT_3D ( 'NONE', #5317, #6040, #8105 ) ;
#9204=FACE_OUTER_BOUND ( 'NONE', #3065, .T. ) ;
#9208=EDGE_CURVE ( 'NONE', #8845, #4499, #8714, .T. ) ;
#9222=ADVANCED_FACE ( 'NONE', ( #1042 ), #185, .F. ) ;
#9223=DIRECTION ( 'NONE',  ( 0.000000000000000000, 0.000000000000000000, 1.000000000000000000 ) ) ;
#9227=ORIENTED_EDGE ( 'NONE', *, *, #3589, .F. ) ;
#9244=CARTESIAN_POINT ( 'NONE',  ( -16.50000000000000000, 7.347880794884123680E-16, 5.000000000000000000 ) ) ;
#9248=CIRCLE ( 'NONE', #3269, 14.49999999999998401 ) ;
#9258=LINE ( 'NONE', #5723, #4805 ) ;
#9259=CARTESIAN_POINT ( 'NONE',  ( 7.180166011355011868, 26.02777777777776791, 0.000000000000000000 ) ) ;
#9260=ORIENTED_EDGE ( 'NONE', *, *, #774, .T. ) ;
#9261=VERTEX_POINT ( 'NONE', #9148 ) ;
#9266=AXIS2_PLACEMENT_3D ( 'NONE', #4802, #5624, #5847 ) ;
#9276=PRODUCT_DEFINITION_FORMATION_WITH_SPECIFIED_SOURCE ( 'ANY', '', #2705, .NOT_KNOWN. ) ;
#9277=CARTESIAN_POINT ( 'NONE',  ( 0.000000000000000000, -22.50000000000000355, 10.00000000000000000 ) ) ;
#9278=FACE_OUTER_BOUND ( 'NONE', #7765, .T. ) ;
#9282=AXIS2_PLACEMENT_3D ( 'NONE', #7818, #6431, #6477 ) ;
#9283=CARTESIAN_POINT ( 'NONE',  ( 0.000000000000000000, 22.50000000000000355, 10.00000000000000000 ) ) ;
#9314=CIRCLE ( 'NONE', #5181, 8.000000000000047962 ) ;
#9320=EDGE_CURVE ( 'NONE', #7086, #3688, #1810, .T. ) ;
#9322=CARTESIAN_POINT ( 'NONE',  ( -28.40723282374007752, -2.660173739710364416, 1.529649672404344241 ) ) ;
#9342=ORIENTED_EDGE ( 'NONE', *, *, #4297, .F. ) ;
#9349=CARTESIAN_POINT ( 'NONE',  ( -30.00000000000000000, 0.000000000000000000, 10.00000000000000000 ) ) ;
#9364=ORIENTED_EDGE ( 'NONE', *, *, #8816, .T. ) ;
#9370=FACE_BOUND ( 'NONE', #6909, .T. ) ;
#9373=CARTESIAN_POINT ( 'NONE',  ( -28.10782586465402133, -3.612161042402820765, 1.337173770134741924 ) ) ;
#9387=EDGE_LOOP ( 'NONE', ( #6340, #4993 ) ) ;
#9389=AXIS2_PLACEMENT_3D ( 'NONE', #5152, #9427, #6693 ) ;
#9405=CIRCLE ( 'NONE', #3574, 15.00000000000000000 ) ;
#9408=CARTESIAN_POINT ( 'NONE',  ( 0.000000000000000000, 0.000000000000000000, 0.000000000000000000 ) ) ;
#9412=ORIENTED_EDGE ( 'NONE', *, *, #3222, .F. ) ;
#9414=ADVANCED_FACE ( 'NONE', ( #6426, #2044 ), #4834, .T. ) ;
#9420=CARTESIAN_POINT ( 'NONE',  ( -28.75000000000003553, -0.3373484206894374338, 1.750000000000030642 ) ) ;
#9427=DIRECTION ( 'NONE',  ( 0.000000000000000000, 0.000000000000000000, -1.000000000000000000 ) ) ;
#9431=DIRECTION ( 'NONE',  ( -1.000000000000000000, 0.000000000000000000, 0.000000000000000000 ) ) ;
#9432=ORIENTED_EDGE ( 'NONE', *, *, #9208, .T. ) ;
#9435=VERTEX_POINT ( 'NONE', #3576 ) ;
#9436=EDGE_CURVE ( 'NONE', #2348, #1368, #1457, .T. ) ;
#9447=LINE ( 'NONE', #8059, #8249 ) ;
#9452=DIRECTION ( 'NONE',  ( 1.000000000000000000, 8.881784197001252323E-16, 0.000000000000000000 ) ) ;
#9453=CARTESIAN_POINT ( 'NONE',  ( 0.000000000000000000, 0.000000000000000000, 50.00000000000000000 ) ) ;
#9459=VERTEX_POINT ( 'NONE', #1560 ) ;
#9460=EDGE_CURVE ( 'NONE', #7998, #3455, #404, .T. ) ;
#9466=CONICAL_SURFACE ( 'NONE', #7786, 11.96410161513786008, 0.2617993877991461882 ) ;
#9474=DIRECTION ( 'NONE',  ( 0.000000000000000000, 0.000000000000000000, -1.000000000000000000 ) ) ;
#9523=COLOUR_RGB('Grey',0.48,0.52,0.57);
#9524=FILL_AREA_STYLE_COLOUR('',#9523);
#9525=FILL_AREA_STYLE('',(#9524));
#9526=SURFACE_STYLE_FILL_AREA(#9525);
#9527=SURFACE_SIDE_STYLE('',(#9526));
#9528=SURFACE_STYLE_USAGE(.BOTH.,#9527);
#9529=PRESENTATION_STYLE_ASSIGNMENT((#9528));
ENDSEC;
END-ISO-10303-21;
